ISO-10303-21;
HEADER;
FILE_DESCRIPTION (('STEP AP203'),
    '1' );
FILE_NAME ('Cleco, Handle, Pivoting.step',
    '2026-10-09T13:45:32',
    ( '' ),
    ( '' ),
    'SwSTEP 2.0',
    'SolidWorks 2024',
    '' );
FILE_SCHEMA (( 'AUTOMOTIVE_DESIGN' ));
ENDSEC;

DATA;
#1=DIRECTION ( 'NONE',  ( -0.6157549048526801405, 0.7879377495398142139, 0.000000000000000000 ) ) ;
#4=ORIENTED_EDGE ( 'NONE', *, *, #5907, .T. ) ;
#5=CARTESIAN_POINT ( 'NONE',  ( 1.850068364776406682, 1.494658567734585608, 0.000000000000000000 ) ) ;
#6=VERTEX_POINT ( 'NONE', #7280 ) ;
#9=CARTESIAN_POINT ( 'NONE',  ( -5.996547682996108186, -1.882193845889704065, 0.2179999999999999993 ) ) ;
#25=AXIS2_PLACEMENT_3D ( 'NONE', #111, #2600, #7606 ) ;
#28=CARTESIAN_POINT ( 'NONE',  ( 1.416570667224800406, 1.056400084382879134, -0.2054632529226294024 ) ) ;
#33=B_SPLINE_CURVE_WITH_KNOTS ( 'NONE', 3,
 ( #1903, #1397, #3941, #5831 ),
 .UNSPECIFIED., .F., .F.,
 ( 4, 4 ),
 ( 0.001688628934469491114, 0.002127673841090521080 ),
 .UNSPECIFIED. ) ;
#35=CARTESIAN_POINT ( 'NONE',  ( -1.204376266962890796, -0.2040480809676099017, 0.2500000000000000000 ) ) ;
#40=CARTESIAN_POINT ( 'NONE',  ( 1.323792169463187340, 1.088966521967518863, -0.1270528182937126493 ) ) ;
#42=CARTESIAN_POINT ( 'NONE',  ( 1.684866161243239846, 1.178252195112418299, -0.1039999999999998703 ) ) ;
#50=ORIENTED_EDGE ( 'NONE', *, *, #1216, .T. ) ;
#53=EDGE_LOOP ( 'NONE', ( #7030, #861, #647, #7343 ) ) ;
#55=DIRECTION ( 'NONE',  ( -1.000000000000000000, 0.000000000000000000, 0.000000000000000000 ) ) ;
#59=ORIENTED_EDGE ( 'NONE', *, *, #2335, .F. ) ;
#60=VECTOR ( 'NONE', #178, 39.37007874015747433 ) ;
#62=DIRECTION ( 'NONE',  ( 0.8639477456102231390, 0.5035814659566147933, -0.000000000000000000 ) ) ;
#63=CIRCLE ( 'NONE', #3353, 0.09999999999999999167 ) ;
#70=CARTESIAN_POINT ( 'NONE',  ( 1.752412446118922995, 1.417229020394738415, 0.1726873346618605365 ) ) ;
#83=DIRECTION ( 'NONE',  ( 0.000000000000000000, 0.000000000000000000, 1.000000000000000000 ) ) ;
#84=DIRECTION ( 'NONE',  ( 0.7879377495398138809, 0.6157549048526804736, 0.000000000000000000 ) ) ;
#90=EDGE_CURVE ( 'NONE', #3501, #7797, #7679, .T. ) ;
#93=DIRECTION ( 'NONE',  ( 0.7879377495398159903, 0.6157549048526775870, -0.000000000000000000 ) ) ;
#98=CIRCLE ( 'NONE', #4156, 6.962657474112426748 ) ;
#100=AXIS2_PLACEMENT_3D ( 'NONE', #6028, #4066, #402 ) ;
#101=FACE_OUTER_BOUND ( 'NONE', #53, .T. ) ;
#105=ORIENTED_EDGE ( 'NONE', *, *, #272, .F. ) ;
#107=FACE_OUTER_BOUND ( 'NONE', #1359, .T. ) ;
#109=CARTESIAN_POINT ( 'NONE',  ( 0.000000000000000000, 0.000000000000000000, 0.2500000000000000000 ) ) ;
#110=CARTESIAN_POINT ( 'NONE',  ( 1.417684048173985634, 1.054372030571947283, -0.2033754655707550874 ) ) ;
#111=CARTESIAN_POINT ( 'NONE',  ( 0.000000000000000000, 0.000000000000000000, 0.2500000000000000000 ) ) ;
#112=VERTEX_POINT ( 'NONE', #7478 ) ;
#115=CARTESIAN_POINT ( 'NONE',  ( 1.832772415705825830, 1.448773774648827617, 0.06821617062301892076 ) ) ;
#120=CARTESIAN_POINT ( 'NONE',  ( 1.380988422957101003, 1.174934410393058126, 0.2179999999999999993 ) ) ;
#123=EDGE_CURVE ( 'NONE', #4974, #3239, #3718, .T. ) ;
#124=ADVANCED_FACE ( 'NONE', ( #549 ), #7584, .F. ) ;
#126=EDGE_CURVE ( 'NONE', #3812, #6, #587, .T. ) ;
#130=CARTESIAN_POINT ( 'NONE',  ( 1.531818848064314453, 1.858671604592519344, -3.087930470258342319E-05 ) ) ;
#134=ORIENTED_EDGE ( 'NONE', *, *, #3394, .F. ) ;
#135=DIRECTION ( 'NONE',  ( 1.000000000000000000, 0.000000000000000000, 0.000000000000000000 ) ) ;
#136=CARTESIAN_POINT ( 'NONE',  ( 1.723350842796532278, 1.129006085766179890, -0.1039999999999998703 ) ) ;
#138=DIRECTION ( 'NONE',  ( -0.4606913525677313603, -0.8875604078987042733, -0.000000000000000000 ) ) ;
#140=VERTEX_POINT ( 'NONE', #3018 ) ;
#152=CARTESIAN_POINT ( 'NONE',  ( 1.792094459600980905, 1.446946837835136890, 0.1263687957420392971 ) ) ;
#156=CARTESIAN_POINT ( 'NONE',  ( -4.882388066182508091, 5.670153330992292240, 0.000000000000000000 ) ) ;
#160=FACE_OUTER_BOUND ( 'NONE', #466, .T. ) ;
#169=DIRECTION ( 'NONE',  ( -0.6157549048526804736, 0.7879377495398138809, 0.000000000000000000 ) ) ;
#174=AXIS2_PLACEMENT_3D ( 'NONE', #7286, #2325, #6791 ) ;
#175=DIRECTION ( 'NONE',  ( -0.6157549048526804736, 0.7879377495398138809, -0.000000000000000000 ) ) ;
#178=DIRECTION ( 'NONE',  ( -0.7879377495398141029, -0.6157549048526802515, 0.000000000000000000 ) ) ;
#179=ADVANCED_FACE ( 'NONE', ( #8043 ), #2438, .T. ) ;
#182=ORIENTED_EDGE ( 'NONE', *, *, #8026, .T. ) ;
#183=CARTESIAN_POINT ( 'NONE',  ( 1.437142212821869380, 1.212327995214701915, 0.2179999999999999993 ) ) ;
#185=CARTESIAN_POINT ( 'NONE',  ( 1.584081668904965046, 1.313867407547560484, 0.2488142415425237675 ) ) ;
#188=CIRCLE ( 'NONE', #3205, 0.1250000000000000000 ) ;
#191=CLOSED_SHELL ( 'NONE', ( #5192, #6881, #1622, #3884, #1222, #3083, #341, #2322, #4646, #2841, #3828, #5309, #3477, #3646, #3790, #635, #4984, #179, #5486, #4337, #4696, #6894, #4687, #1314, #3240, #2939, #7837, #1030, #6205, #3651, #6792, #6797, #4635, #2616, #2625, #3329, #3092, #621, #3082, #5243, #4004, #437, #7292, #1593, #3238, #5295, #4287, #7493, #7092, #5494, #2033, #4935, #4584, #5121, #4592, #5599, #6682, #1830, #4404, #124, #5528, #1872, #6303, #7451, #4098, #414 ) ) ;
#193=EDGE_LOOP ( 'NONE', ( #7590, #4456, #4395, #5162 ) ) ;
#194=CARTESIAN_POINT ( 'NONE',  ( 1.477881298880768357, 1.805595895546355356, 0.1305532412730666392 ) ) ;
#199=CARTESIAN_POINT ( 'NONE',  ( 0.2796912674003787513, -4.528516545235624413, 0.000000000000000000 ) ) ;
#200=TOROIDAL_SURFACE ( 'NONE', #2550, 0.2468203157102362433, 0.03200000000000000067 ) ;
#201=ORIENTED_EDGE ( 'NONE', *, *, #4988, .T. ) ;
#207=ORIENTED_EDGE ( 'NONE', *, *, #5593, .T. ) ;
#218=DIRECTION ( 'NONE',  ( 0.6157549048526804736, -0.7879377495398138809, -0.000000000000000000 ) ) ;
#222=ORIENTED_EDGE ( 'NONE', *, *, #3824, .T. ) ;
#225=VERTEX_POINT ( 'NONE', #7448 ) ;
#231=EDGE_CURVE ( 'NONE', #1921, #3782, #676, .T. ) ;
#232=CARTESIAN_POINT ( 'NONE',  ( 1.731490805950789191, 1.384744806415751484, 0.1971537411645175319 ) ) ;
#237=DIRECTION ( 'NONE',  ( -1.000000000000000000, 0.000000000000000000, 0.000000000000000000 ) ) ;
#241=CARTESIAN_POINT ( 'NONE',  ( 1.296168929684020199, 1.702605512879020955, 0.2124775937629295175 ) ) ;
#244=ORIENTED_EDGE ( 'NONE', *, *, #7043, .T. ) ;
#247=EDGE_LOOP ( 'NONE', ( #7423, #3661, #721, #3628 ) ) ;
#252=ORIENTED_EDGE ( 'NONE', *, *, #2079, .F. ) ;
#253=CARTESIAN_POINT ( 'NONE',  ( 0.3566525292043903339, -0.3408511508279103985, 0.2179999999999999993 ) ) ;
#254=CARTESIAN_POINT ( 'NONE',  ( 1.556400554713971651, 1.293514327272109687, 0.2500000000000000000 ) ) ;
#260=CARTESIAN_POINT ( 'NONE',  ( -6.420602001755994159, -1.404684638105634820, 0.3125000000000000000 ) ) ;
#261=DIRECTION ( 'NONE',  ( -0.6157549048526801405, 0.7879377495398141029, 0.000000000000000000 ) ) ;
#266=ORIENTED_EDGE ( 'NONE', *, *, #7875, .T. ) ;
#267=DIRECTION ( 'NONE',  ( 1.000000000000000000, 0.000000000000000000, 0.000000000000000000 ) ) ;
#272=EDGE_CURVE ( 'NONE', #2232, #1125, #6871, .T. ) ;
#273=CARTESIAN_POINT ( 'NONE',  ( 0.9887166869077884668, 0.8277708867933829540, 0.2179999999999999993 ) ) ;
#274=ORIENTED_EDGE ( 'NONE', *, *, #3349, .T. ) ;
#276=ORIENTED_EDGE ( 'NONE', *, *, #636, .F. ) ;
#279=CARTESIAN_POINT ( 'NONE',  ( 1.806702786482898393, 1.440892520688004552, 0.1183513045165567601 ) ) ;
#280=EDGE_CURVE ( 'NONE', #7184, #7717, #6454, .T. ) ;
#283=FACE_OUTER_BOUND ( 'NONE', #2655, .T. ) ;
#292=AXIS2_PLACEMENT_3D ( 'NONE', #5652, #7572, #690 ) ;
#293=CARTESIAN_POINT ( 'NONE',  ( 1.490755817305508879, 1.854670610081086579, -0.01917321476376811912 ) ) ;
#296=CIRCLE ( 'NONE', #818, 0.2819999999999998619 ) ;
#299=FACE_OUTER_BOUND ( 'NONE', #4719, .T. ) ;
#302=CARTESIAN_POINT ( 'NONE',  ( 1.855589205864664581, 1.487096013276917539, -0.0009044316923897459349 ) ) ;
#306=TOROIDAL_SURFACE ( 'NONE', #2004, 0.2819999999999999729, 0.03200000000000000067 ) ;
#314=AXIS2_PLACEMENT_3D ( 'NONE', #9, #2546, #7556 ) ;
#315=CARTESIAN_POINT ( 'NONE',  ( 1.283086085828156087, 1.692381576688154032, -0.1039999999999998703 ) ) ;
#320=CIRCLE ( 'NONE', #6999, 0.06249999999999995143 ) ;
#321=CARTESIAN_POINT ( 'NONE',  ( 1.084347339223417528, 1.496459553539972287, -0.2249973011472257700 ) ) ;
#322=DIRECTION ( 'NONE',  ( 0.6157549048526804736, -0.7879377495398138809, -0.000000000000000000 ) ) ;
#325=DIRECTION ( 'NONE',  ( -0.9456454288325600865, 0.000000000000000000, -0.3251995124966879924 ) ) ;
#327=AXIS2_PLACEMENT_3D ( 'NONE', #1187, #5657, #7420 ) ;
#332=DIRECTION ( 'NONE',  ( -1.000000000000000000, 0.000000000000000000, 0.000000000000000000 ) ) ;
#333=VECTOR ( 'NONE', #2009, 39.37007874015748143 ) ;
#335=ORIENTED_EDGE ( 'NONE', *, *, #3688, .F. ) ;
#336=EDGE_CURVE ( 'NONE', #6943, #6563, #5437, .T. ) ;
#337=CARTESIAN_POINT ( 'NONE',  ( 0.3210248607526589026, -0.3692027715755950013, 0.2472403127172056181 ) ) ;
#338=CARTESIAN_POINT ( 'NONE',  ( 0.1028096983035134415, -0.4582465879184300372, 0.2500000000000000000 ) ) ;
#341=ADVANCED_FACE ( 'NONE', ( #7683 ), #200, .T. ) ;
#345=LENGTH_MEASURE_WITH_UNIT ( LENGTH_MEASURE( 0.02539999999999999897 ), #1907 );
#350=CARTESIAN_POINT ( 'NONE',  ( 15385.85750733448185, -19684.85311172583170, -0.1039999999999998703 ) ) ;
#351=CIRCLE ( 'NONE', #2179, 0.2468203157102362155 ) ;
#352=ORIENTED_EDGE ( 'NONE', *, *, #4135, .T. ) ;
#354=AXIS2_PLACEMENT_3D ( 'NONE', #4407, #5668, #4282 ) ;
#357=CARTESIAN_POINT ( 'NONE',  ( 1.564847234473322191, 1.084460213605131562, -0.1039999999999998287 ) ) ;
#361=AXIS2_PLACEMENT_3D ( 'NONE', #4371, #138, #1976 ) ;
#362=CYLINDRICAL_SURFACE ( 'NONE', #4659, 6.930657474112426719 ) ;
#368=CARTESIAN_POINT ( 'NONE',  ( 1.541131807373560481, 1.853425921617674055, -0.1039999999999998703 ) ) ;
#371=DIRECTION ( 'NONE',  ( 0.7879377495398135478, 0.6157549048526808066, -8.018138685402973822E-15 ) ) ;
#372=DIRECTION ( 'NONE',  ( -0.000000000000000000, -0.000000000000000000, -1.000000000000000000 ) ) ;
#374=EDGE_CURVE ( 'NONE', #4623, #2262, #3871, .T. ) ;
#380=CARTESIAN_POINT ( 'NONE',  ( 1.862448717126987230, 1.453454210458644313, -0.02693779816119638154 ) ) ;
#396=CARTESIAN_POINT ( 'NONE',  ( 1.240314151020238898, 1.658956310969642578, 0.2499999999999998890 ) ) ;
#402=DIRECTION ( 'NONE',  ( 1.000000000000000000, 0.000000000000000000, 0.000000000000000000 ) ) ;
#405=FACE_OUTER_BOUND ( 'NONE', #626, .T. ) ;
#407=DIRECTION ( 'NONE',  ( -0.000000000000000000, -0.000000000000000000, -1.000000000000000000 ) ) ;
#414=ADVANCED_FACE ( 'NONE', ( #2265 ), #2758, .T. ) ;
#415=DIRECTION ( 'NONE',  ( -0.000000000000000000, -0.000000000000000000, -1.000000000000000000 ) ) ;
#417=CARTESIAN_POINT ( 'NONE',  ( -1.048931738329093699, -0.7261823758192115230, 0.000000000000000000 ) ) ;
#420=DIRECTION ( 'NONE',  ( 0.7879377495398137699, 0.6157549048526804736, 0.000000000000000000 ) ) ;
#423=AXIS2_PLACEMENT_3D ( 'NONE', #5538, #4231, #4352 ) ;
#426=EDGE_CURVE ( 'NONE', #7900, #6943, #4658, .T. ) ;
#428=EDGE_CURVE ( 'NONE', #7825, #3041, #3475, .T. ) ;
#435=CARTESIAN_POINT ( 'NONE',  ( 1.472401076176925283, 1.200024862702049333, 0.2327880490291289461 ) ) ;
#437=ADVANCED_FACE ( 'NONE', ( #6619 ), #5926, .T. ) ;
#438=EDGE_CURVE ( 'NONE', #2111, #3346, #3289, .T. ) ;
#440=DIRECTION ( 'NONE',  ( -1.000000000000000000, 0.000000000000000000, 0.000000000000000000 ) ) ;
#441=DIRECTION ( 'NONE',  ( 1.000000000000000000, 0.000000000000000000, 0.000000000000000000 ) ) ;
#445=VERTEX_POINT ( 'NONE', #6042 ) ;
#446=ORIENTED_EDGE ( 'NONE', *, *, #729, .T. ) ;
#450=CARTESIAN_POINT ( 'NONE',  ( -1.199607936389694096, -0.2200647844395000330, 0.003922330581862806982 ) ) ;
#461=CIRCLE ( 'NONE', #3865, 0.03200000000000001454 ) ;
#464=CARTESIAN_POINT ( 'NONE',  ( 0.09776754390993486199, -0.4589828842714404611, 0.2234246117937112586 ) ) ;
#466=EDGE_LOOP ( 'NONE', ( #6355, #1368, #7116, #5850 ) ) ;
#473=DIRECTION ( 'NONE',  ( -0.2853335501257686646, 0.9584282785752022971, 0.000000000000000000 ) ) ;
#475=DIRECTION ( 'NONE',  ( 0.000000000000000000, 0.000000000000000000, -1.000000000000000000 ) ) ;
#478=CIRCLE ( 'NONE', #3624, 6.930657474112426719 ) ;
#480=CARTESIAN_POINT ( 'NONE',  ( 1.569663840435087332, 1.236826606985905519, 0.1968643041809139405 ) ) ;
#481=CARTESIAN_POINT ( 'NONE',  ( -4.882388066182508091, 5.670153330992292240, 0.03199999999999999373 ) ) ;
#482=EDGE_CURVE ( 'NONE', #5571, #5067, #6879, .T. ) ;
#485=CIRCLE ( 'NONE', #8063, 0.5000000000000279776 ) ;
#487=DIRECTION ( 'NONE',  ( -0.6157549048526803626, 0.7879377495398141029, -0.000000000000000000 ) ) ;
#490=EDGE_LOOP ( 'NONE', ( #1027, #4132, #2110, #7205 ) ) ;
#494=DIRECTION ( 'NONE',  ( 0.000000000000000000, 0.000000000000000000, 1.000000000000000000 ) ) ;
#498=CARTESIAN_POINT ( 'NONE',  ( 1.846835003037430534, 1.498370261438588313, 0.2500000000000000000 ) ) ;
#499=CARTESIAN_POINT ( 'NONE',  ( 1.082008577329383270, 0.9412886604515813271, 0.000000000000000000 ) ) ;
#500=CARTESIAN_POINT ( 'NONE',  ( 1.584026930697933766, 1.313829542709616272, 0.2488199491279635966 ) ) ;
#506=DIRECTION ( 'NONE',  ( -0.7879377495398141029, -0.6157549048526801405, -7.102804783527083974E-15 ) ) ;
#508=CARTESIAN_POINT ( 'NONE',  ( 1.501632106627864172, 1.101688700216157502, 0.2499999999999998335 ) ) ;
#516=CARTESIAN_POINT ( 'NONE',  ( 1.533263802984024204, 1.243817105212362328, 0.2362054852279182326 ) ) ;
#518=VERTEX_POINT ( 'NONE', #1574 ) ;
#520=CARTESIAN_POINT ( 'NONE',  ( 1.299553592491851761, 1.066832042848483653, -0.05797701948372137315 ) ) ;
#528=EDGE_CURVE ( 'NONE', #2262, #7983, #5913, .T. ) ;
#529=DIRECTION ( 'NONE',  ( 0.6157549048561230531, -0.7879377495371234774, 0.000000000000000000 ) ) ;
#536=CARTESIAN_POINT ( 'NONE',  ( 1.669934150624661440, 1.364734201194776286, 0.2262543876504554130 ) ) ;
#538=DIRECTION ( 'NONE',  ( 0.7879377495398138809, 0.6157549048526802515, 0.000000000000000000 ) ) ;
#541=CARTESIAN_POINT ( 'NONE',  ( 1.723350842796532278, 1.129006085766179890, -0.1039999999999998703 ) ) ;
#549=FACE_OUTER_BOUND ( 'NONE', #7220, .T. ) ;
#550=AXIS2_PLACEMENT_3D ( 'NONE', #1792, #4787, #4743 ) ;
#552=CARTESIAN_POINT ( 'NONE',  ( 1.602182050848640182, 1.261380129295977648, 0.2011192772941635953 ) ) ;
#555=ORIENTED_EDGE ( 'NONE', *, *, #884, .F. ) ;
#557=PLANE ( 'NONE',  #1790 ) ;
#559=ORIENTED_EDGE ( 'NONE', *, *, #5593, .F. ) ;
#571=ORIENTED_EDGE ( 'NONE', *, *, #1578, .T. ) ;
#575=AXIS2_PLACEMENT_3D ( 'NONE', #6975, #1395, #4409 ) ;
#576=EDGE_CURVE ( 'NONE', #2354, #2564, #63, .T. ) ;
#577=VERTEX_POINT ( 'NONE', #5471 ) ;
#579=CARTESIAN_POINT ( 'NONE',  ( 1.848231205201100513, 1.461457015412791716, 0.03105351328329579094 ) ) ;
#587=CIRCLE ( 'NONE', #3993, 0.1250000000000000000 ) ;
#592=CARTESIAN_POINT ( 'NONE',  ( 0.009791616623485311505, -0.4636505048871231160, 0.003820833004121301866 ) ) ;
#595=CARTESIAN_POINT ( 'NONE',  ( 1.842690855593505317, 1.503127479225555785, 6.120881109992683290E-14 ) ) ;
#604=DIRECTION ( 'NONE',  ( -0.9726399823210830631, -0.2323175946639496336, 0.000000000000000000 ) ) ;
#606=CARTESIAN_POINT ( 'NONE',  ( 1.723083782080649939, 1.395997476760423961, 0.1965221205739769994 ) ) ;
#609=CARTESIAN_POINT ( 'NONE',  ( 1.600980465589876944, 1.204709832745134657, 0.1951356537883363329 ) ) ;
#611=AXIS2_PLACEMENT_3D ( 'NONE', #5435, #475, #6139 ) ;
#617=ORIENTED_EDGE ( 'NONE', *, *, #5992, .F. ) ;
#621=ADVANCED_FACE ( 'NONE', ( #4239 ), #8034, .T. ) ;
#623=ORIENTED_EDGE ( 'NONE', *, *, #5945, .T. ) ;
#625=AXIS2_PLACEMENT_3D ( 'NONE', #5114, #5818, #5706 ) ;
#626=EDGE_LOOP ( 'NONE', ( #4, #893, #3243, #6088, #4823 ) ) ;
#635=ADVANCED_FACE ( 'NONE', ( #8075 ), #6236, .F. ) ;
#636=EDGE_CURVE ( 'NONE', #140, #3222, #3668, .T. ) ;
#638=CARTESIAN_POINT ( 'NONE',  ( 1.150973126671910540, 0.8530396325060728424, -0.3750000000000000555 ) ) ;
#642=DIRECTION ( 'NONE',  ( -0.8875604078987033851, 0.4606913525677331367, 0.000000000000000000 ) ) ;
#647=ORIENTED_EDGE ( 'NONE', *, *, #2335, .T. ) ;
#650=DIRECTION ( 'NONE',  ( -0.6157549048526823610, 0.7879377495398123266, 0.000000000000000000 ) ) ;
#651=EDGE_LOOP ( 'NONE', ( #2721, #1905, #2051, #7914, #1897, #7051, #4383, #3537 ) ) ;
#653=EDGE_LOOP ( 'NONE', ( #3292, #4215, #3792, #3302 ) ) ;
#659=DIRECTION ( 'NONE',  ( -0.7879377495398141029, -0.6157549048526800295, 0.000000000000000000 ) ) ;
#673=CARTESIAN_POINT ( 'NONE',  ( 0.09770155834983287879, -0.4589921552484208522, 0.02653900339155101928 ) ) ;
#676=LINE ( 'NONE', #2631, #5037 ) ;
#683=CARTESIAN_POINT ( 'NONE',  ( 0.9887166869077879117, 0.8277708867933823988, 0.2179999999999999993 ) ) ;
#684=VERTEX_POINT ( 'NONE', #2618 ) ;
#690=DIRECTION ( 'NONE',  ( 1.000000000000000000, 0.000000000000000000, 0.000000000000000000 ) ) ;
#695=VERTEX_POINT ( 'NONE', #5752 ) ;
#696=LINE ( 'NONE', #35, #1509 ) ;
#703=DIRECTION ( 'NONE',  ( 0.7879377495398138809, 0.6157549048526804736, 0.000000000000000000 ) ) ;
#705=AXIS2_PLACEMENT_3D ( 'NONE', #4868, #7365, #4259 ) ;
#706=DIRECTION ( 'NONE',  ( -0.000000000000000000, -0.000000000000000000, 1.000000000000000000 ) ) ;
#714=LINE ( 'NONE', #5722, #7514 ) ;
#716=DIRECTION ( 'NONE',  ( -0.9726399823210832851, -0.2323175946639495226, -4.958252772465767332E-16 ) ) ;
#717=ORIENTED_EDGE ( 'NONE', *, *, #7786, .F. ) ;
#721=ORIENTED_EDGE ( 'NONE', *, *, #4440, .F. ) ;
#725=CARTESIAN_POINT ( 'NONE',  ( 1.566033889679777413, 1.280741487518077371, 0.2500000000000000555 ) ) ;
#729=EDGE_CURVE ( 'NONE', #518, #2698, #3359, .T. ) ;
#730=CYLINDRICAL_SURFACE ( 'NONE', #8013, 0.3243589946935200308 ) ;
#732=EDGE_CURVE ( 'NONE', #5878, #4081, #2960, .T. ) ;
#734=CARTESIAN_POINT ( 'NONE',  ( 1.855189785566745853, 1.467426056222693953, 0.009546785084580650116 ) ) ;
#739=CARTESIAN_POINT ( 'NONE',  ( 1.251261725424357429, 1.073556033307649704, -0.06746410551919426735 ) ) ;
#743=CARTESIAN_POINT ( 'NONE',  ( -1.040997396242601791, -0.7528336330030669377, 0.2179999999999999993 ) ) ;
#751=CARTESIAN_POINT ( 'NONE',  ( 1.735403701365888285, 1.408497115441140757, 0.2316522750339969627 ) ) ;
#753=AXIS2_PLACEMENT_3D ( 'NONE', #889, #7155, #2264 ) ;
#760=ORIENTED_EDGE ( 'NONE', *, *, #780, .F. ) ;
#765=CARTESIAN_POINT ( 'NONE',  ( 1.592784593561623607, 1.300866851810909886, 0.2489796966440675774 ) ) ;
#771=CARTESIAN_POINT ( 'NONE',  ( 1.849479720061930399, 1.475133735913631616, 0.03415326110672887300 ) ) ;
#778=CARTESIAN_POINT ( 'NONE',  ( 1.552296370367317158, 1.257885440169557612, 0.2367010496530764507 ) ) ;
#780=EDGE_CURVE ( 'NONE', #6611, #6939, #33, .T. ) ;
#781=EDGE_CURVE ( 'NONE', #4837, #7187, #5801, .T. ) ;
#784=CARTESIAN_POINT ( 'NONE',  ( 1.437142212823555587, 1.212327995211809117, 0.2500000000000000000 ) ) ;
#787=VERTEX_POINT ( 'NONE', #2664 ) ;
#788=B_SPLINE_CURVE_WITH_KNOTS ( 'NONE', 3,
 ( #3831, #2630, #1405, #5724, #793, #891 ),
 .UNSPECIFIED., .F., .F.,
 ( 4, 2, 4 ),
 ( 0.0008157146336201673373, 0.007786668999356947084, 0.01475762336509372705 ),
 .UNSPECIFIED. ) ;
#793=CARTESIAN_POINT ( 'NONE',  ( 1.821163076082948917, 1.492795972680864169, -0.07459452442999962851 ) ) ;
#799=ORIENTED_EDGE ( 'NONE', *, *, #5540, .F. ) ;
#800=DIRECTION ( 'NONE',  ( -0.6157549048526697044, 0.7879377495398223186, 0.000000000000000000 ) ) ;
#803=B_SPLINE_CURVE_WITH_KNOTS ( 'NONE', 3,
 ( #1064, #1682, #2833, #7788 ),
 .UNSPECIFIED., .F., .F.,
 ( 4, 4 ),
 ( 0.000000000000000000, 0.001713611390986142201 ),
 .UNSPECIFIED. ) ;
#806=CARTESIAN_POINT ( 'NONE',  ( 1.761728046479479337, 1.406920720071850539, 0.1725519765195418775 ) ) ;
#808=DIRECTION ( 'NONE',  ( -0.7879377495398141029, -0.6157549048526800295, 0.000000000000000000 ) ) ;
#810=VERTEX_POINT ( 'NONE', #3168 ) ;
#812=CARTESIAN_POINT ( 'NONE',  ( 0.3037072441740230055, -0.3811681129206500596, 8.812699745186523597E-17 ) ) ;
#818=AXIS2_PLACEMENT_3D ( 'NONE', #2222, #372, #1038 ) ;
#822=VERTEX_POINT ( 'NONE', #955 ) ;
#823=EDGE_CURVE ( 'NONE', #4706, #787, #5910, .T. ) ;
#826=CARTESIAN_POINT ( 'NONE',  ( 1.400692579912386826, 1.149720402407784059, 0.2179999999999999438 ) ) ;
#829=EDGE_CURVE ( 'NONE', #4837, #3183, #2082, .T. ) ;
#833=AXIS2_PLACEMENT_3D ( 'NONE', #2345, #4971, #506 ) ;
#834=CARTESIAN_POINT ( 'NONE',  ( 1.684866161243239846, 1.178252195112418299, -0.1039999999999998703 ) ) ;
#843=AXIS2_PLACEMENT_3D ( 'NONE', #5806, #1370, #2637 ) ;
#849=CARTESIAN_POINT ( 'NONE',  ( 1.726550314240142381, 1.368787266291294991, 0.1934252906403959582 ) ) ;
#854=CARTESIAN_POINT ( 'NONE',  ( 0.2796912674001651444, -4.528516545235133250, -0.05999999999999999778 ) ) ;
#858=CARTESIAN_POINT ( 'NONE',  ( 1.840267422809780173, 1.485682443985806067, 0.03416929312143927866 ) ) ;
#859=CARTESIAN_POINT ( 'NONE',  ( -1.499610808650658100, -1.013166758633947007, 0.3125000000000000000 ) ) ;
#861=ORIENTED_EDGE ( 'NONE', *, *, #4938, .T. ) ;
#862=CARTESIAN_POINT ( 'NONE',  ( 1.301676237712382722, 1.089389786036094376, -0.1088174584421244540 ) ) ;
#863=CARTESIAN_POINT ( 'NONE',  ( 0.3210139061311759745, -0.3692105794741389335, 0.002757220755949914542 ) ) ;
#866=CARTESIAN_POINT ( 'NONE',  ( 1.107456280057753872, 1.514518649799285299, -0.2121970708455140908 ) ) ;
#872=EDGE_CURVE ( 'NONE', #445, #1342, #6505, .T. ) ;
#882=EDGE_CURVE ( 'NONE', #6669, #6611, #6240, .T. ) ;
#884=EDGE_CURVE ( 'NONE', #4081, #6939, #2040, .T. ) ;
#889=CARTESIAN_POINT ( 'NONE',  ( -4.882388066182516084, 5.670153330992327767, 0.3125000000000000000 ) ) ;
#891=CARTESIAN_POINT ( 'NONE',  ( 1.877688265130482037, 1.420950500079102286, -0.07807135826935437950 ) ) ;
#893=ORIENTED_EDGE ( 'NONE', *, *, #3081, .T. ) ;
#899=EDGE_CURVE ( 'NONE', #3428, #1559, #924, .T. ) ;
#906=EDGE_CURVE ( 'NONE', #140, #2262, #7410, .T. ) ;
#907=CARTESIAN_POINT ( 'NONE',  ( 1.664570443216303763, 1.333357566009973905, 0.2227136479326053131 ) ) ;
#912=CARTESIAN_POINT ( 'NONE',  ( 1.494536332678459090, 1.857624994339484470, 0.06788303539822813926 ) ) ;
#917=ORIENTED_EDGE ( 'NONE', *, *, #3885, .F. ) ;
#918=CARTESIAN_POINT ( 'NONE',  ( 1.351681538574651675, 1.071232595603015980, -0.1189673409015081368 ) ) ;
#923=EDGE_LOOP ( 'NONE', ( #5142, #7808, #3442, #6800, #1295 ) ) ;
#924=LINE ( 'NONE', #2186, #5972 ) ;
#927=EDGE_LOOP ( 'NONE', ( #252, #2623, #986, #2339 ) ) ;
#929=CARTESIAN_POINT ( 'NONE',  ( -0.02691660025194390557, -0.4609452288429354838, 0.2500000000000001110 ) ) ;
#931=CARTESIAN_POINT ( 'NONE',  ( -6.110602001756019419, -1.404684638105634820, 0.3125000000000000000 ) ) ;
#937=DIRECTION ( 'NONE',  ( 0.000000000000000000, 0.000000000000000000, -1.000000000000000000 ) ) ;
#942=EDGE_CURVE ( 'NONE', #3574, #2815, #3618, .T. ) ;
#951=CARTESIAN_POINT ( 'NONE',  ( 1.491280890329322872, 1.855080942356710949, -0.01135997346352945678 ) ) ;
#954=AXIS2_PLACEMENT_3D ( 'NONE', #7532, #6384, #1258 ) ;
#955=CARTESIAN_POINT ( 'NONE',  ( -1.204376266962890796, -0.2040480809676099017, 0.03199999999999999373 ) ) ;
#962=ORIENTED_EDGE ( 'NONE', *, *, #2079, .T. ) ;
#966=CARTESIAN_POINT ( 'NONE',  ( 1.142655413120957197, 0.6307864494084283180, 0.03199999999999999373 ) ) ;
#967=CARTESIAN_POINT ( 'NONE',  ( 1.414726328521486387, 1.163888030567411302, 0.2500000000000000000 ) ) ;
#973=AXIS2_PLACEMENT_3D ( 'NONE', #5546, #5591, #1196 ) ;
#979=TOROIDAL_SURFACE ( 'NONE', #5949, 0.2923589946935198913, 0.03200000000000000067 ) ;
#980=CARTESIAN_POINT ( 'NONE',  ( 1.258764021883149731, 1.079418902353951548, -0.03540237178041891197 ) ) ;
#982=ORIENTED_EDGE ( 'NONE', *, *, #4143, .T. ) ;
#984=CARTESIAN_POINT ( 'NONE',  ( 1.536251789383608735, 1.851359936419108676, -0.007784679637053777863 ) ) ;
#986=ORIENTED_EDGE ( 'NONE', *, *, #636, .T. ) ;
#987=DIRECTION ( 'NONE',  ( 0.4606913525677331367, 0.8875604078987031631, 0.000000000000000000 ) ) ;
#995=CARTESIAN_POINT ( 'NONE',  ( -1.204118949239847192, -0.2049124047817365846, 0.02346499912907216642 ) ) ;
#996=CARTESIAN_POINT ( 'NONE',  ( 1.517292316521555051, 1.875408262972374729, -0.04789697820786732035 ) ) ;
#999=ORIENTED_EDGE ( 'NONE', *, *, #123, .F. ) ;
#1001=CARTESIAN_POINT ( 'NONE',  ( 1.503810987132070176, 1.221025632701057795, 0.2329445735574367515 ) ) ;
#1005=CIRCLE ( 'NONE', #7924, 0.3099999999999745737 ) ;
#1006=VERTEX_POINT ( 'NONE', #499 ) ;
#1007=DIRECTION ( 'NONE',  ( 1.000000000000000000, 0.000000000000000000, 0.000000000000000000 ) ) ;
#1008=FACE_OUTER_BOUND ( 'NONE', #6416, .T. ) ;
#1011=ORIENTED_EDGE ( 'NONE', *, *, #6995, .F. ) ;
#1015=CIRCLE ( 'NONE', #2448, 0.03200000000000001454 ) ;
#1016=LINE ( 'NONE', #4702, #7792 ) ;
#1021=CARTESIAN_POINT ( 'NONE',  ( 1.492515782973968363, 1.856045982048426746, -0.05383208248535607116 ) ) ;
#1022=CIRCLE ( 'NONE', #4822, 0.2704878104020023710 ) ;
#1023=AXIS2_PLACEMENT_3D ( 'NONE', #1264, #1885, #3030 ) ;
#1027=ORIENTED_EDGE ( 'NONE', *, *, #5349, .F. ) ;
#1029=EDGE_CURVE ( 'NONE', #5193, #2815, #7982, .T. ) ;
#1030=ADVANCED_FACE ( 'NONE', ( #2369 ), #4275, .F. ) ;
#1034=ORIENTED_EDGE ( 'NONE', *, *, #6551, .F. ) ;
#1038=DIRECTION ( 'NONE',  ( 1.000000000000000000, 0.000000000000000000, 0.000000000000000000 ) ) ;
#1040=EDGE_CURVE ( 'NONE', #3041, #7825, #7665, .T. ) ;
#1044=CARTESIAN_POINT ( 'NONE',  ( 1.417679350985660447, 1.200983401422921704, 0.2500000000000000000 ) ) ;
#1048=VERTEX_POINT ( 'NONE', #1846 ) ;
#1056=DIRECTION ( 'NONE',  ( 0.6157549048526803626, -0.7879377495398141029, 0.000000000000000000 ) ) ;
#1057=CARTESIAN_POINT ( 'NONE',  ( -1.204376266962890796, -0.2040480809676099017, 0.2179999999999999993 ) ) ;
#1060=ORIENTED_EDGE ( 'NONE', *, *, #1531, .T. ) ;
#1062=CARTESIAN_POINT ( 'NONE',  ( -4.521705384338368994, -3.437882612028420048, 0.2179999999999999993 ) ) ;
#1064=CARTESIAN_POINT ( 'NONE',  ( 1.380988422954957606, 1.174934410395800821, 0.2500000000000000000 ) ) ;
#1067=CARTESIAN_POINT ( 'NONE',  ( -1.222146065255383940, -0.1443597716867830172, 0.3125000000000000000 ) ) ;
#1075=CARTESIAN_POINT ( 'NONE',  ( 0.09911377505692577083, -0.4587915400498679963, 0.2226707364275206102 ) ) ;
#1079=VERTEX_POINT ( 'NONE', #3735 ) ;
#1087=CARTESIAN_POINT ( 'NONE',  ( 1.288127153466032349, 1.061753156913864515, -0.04562500015858166058 ) ) ;
#1093=EDGE_LOOP ( 'NONE', ( #6163, #7798, #6038, #6708 ) ) ;
#1099=AXIS2_PLACEMENT_3D ( 'NONE', #1785, #3757, #3638 ) ;
#1108=CARTESIAN_POINT ( 'NONE',  ( 1.721454941643402181, 1.365050579745590298, 0.1970682748494993752 ) ) ;
#1124=DIRECTION ( 'NONE',  ( 0.6157549048526823610, -0.7879377495398123266, 0.000000000000000000 ) ) ;
#1125=VERTEX_POINT ( 'NONE', #4509 ) ;
#1127=EDGE_CURVE ( 'NONE', #3019, #4660, #3572, .T. ) ;
#1128=CARTESIAN_POINT ( 'NONE',  ( 1.298294415927210732, 1.066201332570530402, -0.05662632202991332159 ) ) ;
#1130=CARTESIAN_POINT ( 'NONE',  ( 1.892615878912688121, 1.261282748826759059, -0.1039999999999998703 ) ) ;
#1134=CARTESIAN_POINT ( 'NONE',  ( 1.879749225811877533, 1.418330869987895593, -0.07819788172161412643 ) ) ;
#1135=ORIENTED_EDGE ( 'NONE', *, *, #1127, .F. ) ;
#1138=CIRCLE ( 'NONE', #7419, 0.03200000000000009781 ) ;
#1139=CARTESIAN_POINT ( 'NONE',  ( 1.631407451075704174, 1.225884142284358269, 0.1986297663929937618 ) ) ;
#1141=EDGE_CURVE ( 'NONE', #5314, #1559, #7503, .T. ) ;
#1144=FACE_OUTER_BOUND ( 'NONE', #927, .T. ) ;
#1149=CIRCLE ( 'NONE', #4413, 0.3243589946935201418 ) ;
#1151=CARTESIAN_POINT ( 'NONE',  ( 1.804885088013157501, 1.272044176619705036, -0.1039999999999998703 ) ) ;
#1160=LINE ( 'NONE', #4317, #3059 ) ;
#1166=DIRECTION ( 'NONE',  ( -0.7879377495398141029, -0.6157549048526801405, 0.000000000000000000 ) ) ;
#1168=CARTESIAN_POINT ( 'NONE',  ( 1.414905630928118274, 1.059296705655214499, -0.2064098076014010408 ) ) ;
#1169=CARTESIAN_POINT ( 'NONE',  ( 1.821814260629908144, 1.491972579020843792, -0.07464810438835918494 ) ) ;
#1170=CARTESIAN_POINT ( 'NONE',  ( 1.449232787663330191, 1.184861245930724838, 0.2316522750340390402 ) ) ;
#1172=PLANE ( 'NONE',  #174 ) ;
#1174=EDGE_LOOP ( 'NONE', ( #276, #7729, #4961, #982 ) ) ;
#1182=ORIENTED_EDGE ( 'NONE', *, *, #4192, .T. ) ;
#1186=EDGE_CURVE ( 'NONE', #1576, #3933, #6108, .T. ) ;
#1187=CARTESIAN_POINT ( 'NONE',  ( 0.8135394388118154518, 1.284829519253825492, -0.3750000000000000555 ) ) ;
#1194=CARTESIAN_POINT ( 'NONE',  ( 1.101712734284013395, 0.9160746524671463664, 0.03199999999999999373 ) ) ;
#1195=CARTESIAN_POINT ( 'NONE',  ( 1.859753234433174418, 1.471617347716406288, -0.009971652696953780398 ) ) ;
#1196=DIRECTION ( 'NONE',  ( -0.6157549048526697044, 0.7879377495398223186, 0.000000000000000000 ) ) ;
#1197=CARTESIAN_POINT ( 'NONE',  ( -1.047725383040473579, -0.7302344931468570666, 0.2500000000000000555 ) ) ;
#1202=LINE ( 'NONE', #2387, #3603 ) ;
#1203=CARTESIAN_POINT ( 'NONE',  ( 0.2796912674001651444, -4.528516545235133250, 0.3125000000000000000 ) ) ;
#1204=CARTESIAN_POINT ( 'NONE',  ( 0.07611279676787391368, -0.4615777240268290615, 0.01842339291575492005 ) ) ;
#1207=CARTESIAN_POINT ( 'NONE',  ( 1.676600392854198152, 1.675569901472168111, -0.06304405137341999310 ) ) ;
#1208=AXIS2_PLACEMENT_3D ( 'NONE', #5107, #6276, #650 ) ;
#1210=CARTESIAN_POINT ( 'NONE',  ( 1.681471845429138634, 1.360654782462170198, 0.2349444525762485469 ) ) ;
#1211=PRODUCT_DEFINITION_FORMATION_WITH_SPECIFIED_SOURCE ( 'ANY', '', #4024, .NOT_KNOWN. ) ;
#1216=EDGE_CURVE ( 'NONE', #1079, #5222, #351, .T. ) ;
#1217=CARTESIAN_POINT ( 'NONE',  ( 1.812419000491751309, 1.462705014722680996, 0.09539854745190586016 ) ) ;
#1218=VERTEX_POINT ( 'NONE', #7010 ) ;
#1219=AXIS2_PLACEMENT_3D ( 'NONE', #980, #4058, #7849 ) ;
#1222=ADVANCED_FACE ( 'NONE', ( #7660 ), #7021, .F. ) ;
#1224=ORIENTED_EDGE ( 'NONE', *, *, #6688, .T. ) ;
#1226=CARTESIAN_POINT ( 'NONE',  ( 1.571814533976804151, 1.273076930690908437, 0.2372021369714001904 ) ) ;
#1228=EDGE_LOOP ( 'NONE', ( #2359, #4248, #5874, #105 ) ) ;
#1229=DIRECTION ( 'NONE',  ( -0.6021462665530982195, 0.7983857925064579142, 0.000000000000000000 ) ) ;
#1232=CARTESIAN_POINT ( 'NONE',  ( 1.697621308141715746, 1.379869104482623454, 0.2130385109652204456 ) ) ;
#1240=DIRECTION ( 'NONE',  ( -0.7879377495398141029, -0.6157549048526800295, -0.000000000000000000 ) ) ;
#1245=DIRECTION ( 'NONE',  ( 0.000000000000000000, 0.000000000000000000, 1.000000000000000000 ) ) ;
#1246=DIRECTION ( 'NONE',  ( 0.000000000000000000, 0.000000000000000000, -1.000000000000000000 ) ) ;
#1247=DIRECTION ( 'NONE',  ( -0.7879377495398138809, -0.6157549048526803626, 0.000000000000000000 ) ) ;
#1249=DIRECTION ( 'NONE',  ( -0.4606913525677331367, -0.8875604078987033851, 0.000000000000000000 ) ) ;
#1250=CARTESIAN_POINT ( 'NONE',  ( 0.000000000000000000, 0.000000000000000000, 0.000000000000000000 ) ) ;
#1253=AXIS2_PLACEMENT_3D ( 'NONE', #7049, #7577, #1422 ) ;
#1257=B_SPLINE_CURVE_WITH_KNOTS ( 'NONE', 3,
 ( #5005, #3619, #500, #7505, #7467, #6849, #536, #1232, #5502, #8066 ),
 .UNSPECIFIED., .F., .F.,
 ( 4, 2, 2, 2, 4 ),
 ( 0.000000000000000000, 0.001297014371279050018, 0.002594028742558100037, 0.003891043113837150055, 0.005188057485116200074 ),
 .UNSPECIFIED. ) ;
#1258=DIRECTION ( 'NONE',  ( -0.8875604078987042733, 0.4606913525677314158, 0.000000000000000000 ) ) ;
#1259=ORIENTED_EDGE ( 'NONE', *, *, #4440, .T. ) ;
#1260=DIRECTION ( 'NONE',  ( -0.6157549048526802515, 0.7879377495398139919, -0.000000000000000000 ) ) ;
#1264=CARTESIAN_POINT ( 'NONE',  ( 2.010976737284365878, 1.235749360019309684, -0.08212881570848259982 ) ) ;
#1269=VECTOR ( 'NONE', #3694, 39.37007874015748143 ) ;
#1274=EDGE_CURVE ( 'NONE', #3903, #7063, #8051, .T. ) ;
#1275=EDGE_CURVE ( 'NONE', #3595, #3574, #4992, .T. ) ;
#1277=CARTESIAN_POINT ( 'NONE',  ( 1.550255360611296540, 0.8757063900986424843, -0.08212881570848257207 ) ) ;
#1280=CARTESIAN_POINT ( 'NONE',  ( 1.414905630928118274, 1.059296705655214499, -0.2064098076014010408 ) ) ;
#1283=CARTESIAN_POINT ( 'NONE',  ( 1.537918127343594454, 1.852987194258524983, 0.000000000000000000 ) ) ;
#1285=ORIENTED_EDGE ( 'NONE', *, *, #4841, .F. ) ;
#1290=CARTESIAN_POINT ( 'NONE',  ( 1.580248108977379884, 1.266138851169832380, -0.1250000000000000278 ) ) ;
#1295=ORIENTED_EDGE ( 'NONE', *, *, #7243, .F. ) ;
#1299=CARTESIAN_POINT ( 'NONE',  ( 0.8923633780935225079, 0.7607014108325281798, 0.03199999999999999373 ) ) ;
#1300=VERTEX_POINT ( 'NONE', #4062 ) ;
#1306=ORIENTED_EDGE ( 'NONE', *, *, #7243, .T. ) ;
#1307=DIRECTION ( 'NONE',  ( -0.6157549048526802515, 0.7879377495398142139, -0.000000000000000000 ) ) ;
#1309=DIRECTION ( 'NONE',  ( -0.9726399823210830631, -0.2323175946639496336, -0.000000000000000000 ) ) ;
#1314=ADVANCED_FACE ( 'NONE', ( #4630 ), #6431, .F. ) ;
#1320=EDGE_CURVE ( 'NONE', #4105, #3782, #7803, .T. ) ;
#1323=CARTESIAN_POINT ( 'NONE',  ( 0.2796912674003787513, -4.528516545235624413, 0.2179999999999999993 ) ) ;
#1327=ORIENTED_EDGE ( 'NONE', *, *, #5177, .T. ) ;
#1328=EDGE_CURVE ( 'NONE', #787, #3032, #7208, .T. ) ;
#1334=CARTESIAN_POINT ( 'NONE',  ( 1.690678803126011154, 1.376073966722298536, 0.2163527671803432417 ) ) ;
#1337=CARTESIAN_POINT ( 'NONE',  ( 1.800320205903116921, 1.030513867073702183, -0.08212881570848259982 ) ) ;
#1342=VERTEX_POINT ( 'NONE', #6064 ) ;
#1346=ORIENTED_EDGE ( 'NONE', *, *, #3179, .T. ) ;
#1347=CARTESIAN_POINT ( 'NONE',  ( 1.473442587156926775, 1.198637710842282766, 0.2295096657271606944 ) ) ;
#1348=VECTOR ( 'NONE', #4130, 39.37007874015748854 ) ;
#1351=CARTESIAN_POINT ( 'NONE',  ( 1.499442570351851911, 1.861459104221312000, -0.001141387575425446659 ) ) ;
#1353=AXIS2_PLACEMENT_3D ( 'NONE', #3166, #2615, #5056 ) ;
#1354=B_SPLINE_CURVE_WITH_KNOTS ( 'NONE', 3,
 ( #7297, #6835, #6721, #8054, #609, #1676, #3609, #4179, #5492, #2360, #7373, #6763 ),
 .UNSPECIFIED., .F., .F.,
 ( 4, 2, 2, 2, 2, 4 ),
 ( 8.909715784852462421E-15, 0.001906393393842450556, 0.002859590090759231689, 0.003812786787676013256, 0.005719180181509561645, 0.007625573575343111768 ),
 .UNSPECIFIED. ) ;
#1358=TOROIDAL_SURFACE ( 'NONE', #2405, 0.2819999999999999729, 0.03200000000000000067 ) ;
#1359=EDGE_LOOP ( 'NONE', ( #1060, #1818 ) ) ;
#1368=ORIENTED_EDGE ( 'NONE', *, *, #1458, .T. ) ;
#1370=DIRECTION ( 'NONE',  ( 0.6157549048526803626, -0.7879377495398139919, 0.000000000000000000 ) ) ;
#1378=EDGE_LOOP ( 'NONE', ( #7311, #2409, #7432, #799 ) ) ;
#1381=CARTESIAN_POINT ( 'NONE',  ( 1.800774122434213975, 1.436334721442235507, 0.1268433716242569342 ) ) ;
#1383=VECTOR ( 'NONE', #987, 39.37007874015748143 ) ;
#1386=DIRECTION ( 'NONE',  ( 0.9891211992429681521, 0.000000000000000000, 0.1471028660772870089 ) ) ;
#1392=AXIS2_PLACEMENT_3D ( 'NONE', #5240, #5894, #7202 ) ;
#1395=DIRECTION ( 'NONE',  ( 0.000000000000000000, 0.000000000000000000, -1.000000000000000000 ) ) ;
#1397=CARTESIAN_POINT ( 'NONE',  ( 1.877300571085743108, 1.420647526259452897, -0.06641314542006129806 ) ) ;
#1403=DIRECTION ( 'NONE',  ( 0.7879377495398138809, 0.6157549048526802515, 0.000000000000000000 ) ) ;
#1405=CARTESIAN_POINT ( 'NONE',  ( 1.651097472914581088, 1.707757380030753280, -0.06087441991423112042 ) ) ;
#1406=DIRECTION ( 'NONE',  ( 0.6157549048526803626, -0.7879377495398141029, 0.000000000000000000 ) ) ;
#1410=ORIENTED_EDGE ( 'NONE', *, *, #6214, .F. ) ;
#1411=ORIENTED_EDGE ( 'NONE', *, *, #90, .T. ) ;
#1412=EDGE_LOOP ( 'NONE', ( #4053, #7854, #6735, #2100 ) ) ;
#1421=CARTESIAN_POINT ( 'NONE',  ( 1.496141785815785941, 1.858879618380945509, -0.01305819514303249197 ) ) ;
#1422=DIRECTION ( 'NONE',  ( -0.7879377495398142139, -0.6157549048526800295, 0.000000000000000000 ) ) ;
#1426=CARTESIAN_POINT ( 'NONE',  ( 1.294204688232935219, 1.088727781300392827, -0.1026931866138307559 ) ) ;
#1440=EDGE_CURVE ( 'NONE', #2815, #3298, #3620, .T. ) ;
#1453=CARTESIAN_POINT ( 'NONE',  ( 1.719796567415322386, 1.364484731518883498, 0.1975831474265880849 ) ) ;
#1454=( BOUNDED_SURFACE ( )  B_SPLINE_SURFACE ( 3, 2, ( 
 ( #3413, #996, #5300 ),
 ( #6605, #6567, #7857 ),
 ( #5413, #2870, #3564 ),
 ( #951, #1597, #7257 ),
 ( #5997, #2181, #4680 ),
 ( #6646, #5952, #2952 ) ),
 .UNSPECIFIED., .F., .F., .T. ) 
 B_SPLINE_SURFACE_WITH_KNOTS ( ( 4, 2, 4 ),
 ( 3, 3 ),
 ( -1.528269698292117340E-14, 0.0008095007283496732150, 0.001619001456714629127 ),
 ( 0.000000000000000000, 1.000000000000000000 ),
 .UNSPECIFIED. ) 
 GEOMETRIC_REPRESENTATION_ITEM ( )  RATIONAL_B_SPLINE_SURFACE ( (
 ( 1.000000000000000000, 0.7071067811870255237, 1.000000000000000000),
 ( 1.000000000000000000, 0.7102386623011891498, 1.000000000000000000),
 ( 1.000000000000000000, 0.7133082652150437575, 1.000000000000000000),
 ( 1.000000000000000000, 0.7193245599450390770, 1.000000000000000000),
 ( 1.000000000000000000, 0.7222974223247246028, 1.000000000000000000),
 ( 1.000000000000000000, 0.7250243206839943610, 1.000000000000000000) ) ) 
 REPRESENTATION_ITEM ( '' )  SURFACE ( )  );
#1458=EDGE_CURVE ( 'NONE', #810, #5561, #7937, .T. ) ;
#1461=CARTESIAN_POINT ( 'NONE',  ( 1.762871904346776653, 1.395378910334173828, 0.1649876832364386703 ) ) ;
#1465=CYLINDRICAL_SURFACE ( 'NONE', #625, 0.5000000000000279776 ) ;
#1473=CARTESIAN_POINT ( 'NONE',  ( 1.251356423955005015, 1.643685595130192745, 0.2500000000000000000 ) ) ;
#1474=CARTESIAN_POINT ( 'NONE',  ( 1.733157827470031220, 1.373632878362992527, 0.1887011865795288901 ) ) ;
#1483=ORIENTED_EDGE ( 'NONE', *, *, #5349, .T. ) ;
#1495=EDGE_LOOP ( 'NONE', ( #3915, #4320, #4632, #7245 ) ) ;
#1500=CARTESIAN_POINT ( 'NONE',  ( 1.780616048947831098, 1.055727875058976251, -0.08212881570848259982 ) ) ;
#1502=CARTESIAN_POINT ( 'NONE',  ( 1.704817408831214021, 1.367523911545252879, 0.2140310551078935808 ) ) ;
#1504=AXIS2_PLACEMENT_3D ( 'NONE', #3177, #1406, #6372 ) ;
#1509=VECTOR ( 'NONE', #2535, 39.37007874015748143 ) ;
#1510=CARTESIAN_POINT ( 'NONE',  ( 1.440344085072671199, 1.815275021530317279, 0.1087460313510809767 ) ) ;
#1511=CARTESIAN_POINT ( 'NONE',  ( 1.535041889452112285, 1.849375524390286740, -0.03191141767805402707 ) ) ;
#1514=CARTESIAN_POINT ( 'NONE',  ( 0.2796912674001651444, -4.528516545235133250, 0.3125000000000000000 ) ) ;
#1519=DIRECTION ( 'NONE',  ( 0.6157549048526804736, -0.7879377495398138809, -0.000000000000000000 ) ) ;
#1522=EDGE_LOOP ( 'NONE', ( #335, #7864, #5917 ) ) ;
#1524=CIRCLE ( 'NONE', #6116, 0.3024878104020024550 ) ;
#1528=CARTESIAN_POINT ( 'NONE',  ( 1.473750031596730237, 1.199377247893690601, 0.2292416509145525638 ) ) ;
#1529=AXIS2_PLACEMENT_3D ( 'NONE', #4947, #7965, #3640 ) ;
#1531=EDGE_CURVE ( 'NONE', #1125, #2232, #6707, .T. ) ;
#1532=DIRECTION ( 'NONE',  ( 0.000000000000000000, 0.000000000000000000, -1.000000000000000000 ) ) ;
#1533=FACE_OUTER_BOUND ( 'NONE', #3079, .T. ) ;
#1538=EDGE_CURVE ( 'NONE', #5954, #787, #3561, .T. ) ;
#1548=DIRECTION ( 'NONE',  ( 1.000000000000000000, 0.000000000000000000, 0.000000000000000000 ) ) ;
#1554=DIRECTION ( 'NONE',  ( -1.000000000000000000, 0.000000000000000000, -0.000000000000000000 ) ) ;
#1556=CARTESIAN_POINT ( 'NONE',  ( 1.268245620182552935, 1.680784100216294652, 0.2179999999999998883 ) ) ;
#1559=VERTEX_POINT ( 'NONE', #3189 ) ;
#1561=LINE ( 'NONE', #3446, #5690 ) ;
#1562=CARTESIAN_POINT ( 'NONE',  ( 1.975095093049261896, 1.207708695074841909, -0.1039999999999998703 ) ) ;
#1564=ORIENTED_EDGE ( 'NONE', *, *, #7592, .T. ) ;
#1566=CARTESIAN_POINT ( 'NONE',  ( 1.449725606736619543, 1.190739840090658364, 0.2500000000000000000 ) ) ;
#1569=EDGE_CURVE ( 'NONE', #695, #2111, #2627, .T. ) ;
#1570=ORIENTED_EDGE ( 'NONE', *, *, #6143, .F. ) ;
#1574=CARTESIAN_POINT ( 'NONE',  ( -6.420602001755994159, -1.404684638105634820, -0.05999999999999999778 ) ) ;
#1576=VERTEX_POINT ( 'NONE', #6232 ) ;
#1578=EDGE_CURVE ( 'NONE', #3032, #5193, #3305, .T. ) ;
#1579=EDGE_CURVE ( 'NONE', #1342, #3595, #4382, .T. ) ;
#1581=EDGE_CURVE ( 'NONE', #684, #7184, #2119, .T. ) ;
#1588=CARTESIAN_POINT ( 'NONE',  ( 1.800320205903116921, 1.030513867073702183, -0.08212881570848259982 ) ) ;
#1589=DIRECTION ( 'NONE',  ( 0.000000000000000000, 0.000000000000000000, 1.000000000000000000 ) ) ;
#1590=CARTESIAN_POINT ( 'NONE',  ( 0.3265803234075882466, -0.3651282914590817663, 0.004338029470932578714 ) ) ;
#1591=ORIENTED_EDGE ( 'NONE', *, *, #3873, .T. ) ;
#1593=ADVANCED_FACE ( 'NONE', ( #5033 ), #4429, .T. ) ;
#1597=CARTESIAN_POINT ( 'NONE',  ( 1.515492104094517067, 1.874001439105450473, -0.01551275274473707180 ) ) ;
#1602=CARTESIAN_POINT ( 'NONE',  ( 1.491230041056485378, 1.855041204840421232, -0.04518674047500752938 ) ) ;
#1609=CARTESIAN_POINT ( 'NONE',  ( 1.868427082838399311, 1.436511782911442880, -0.04381998756813935969 ) ) ;
#1618=CIRCLE ( 'NONE', #833, 0.3750000000000000555 ) ;
#1619=DIRECTION ( 'NONE',  ( 1.000000000000000000, -8.943549979258001330E-15, 0.000000000000000000 ) ) ;
#1622=ADVANCED_FACE ( 'NONE', ( #6957 ), #6349, .F. ) ;
#1623=CARTESIAN_POINT ( 'NONE',  ( 1.460659702294222928, 1.192157774404229764, 0.2321080476372760493 ) ) ;
#1630=CARTESIAN_POINT ( 'NONE',  ( 1.535339692041459925, 1.850303721083318420, -0.01584850669601754747 ) ) ;
#1632=ORIENTED_EDGE ( 'NONE', *, *, #4203, .T. ) ;
#1635=AXIS2_PLACEMENT_3D ( 'NONE', #7302, #4878, #1760 ) ;
#1636=CARTESIAN_POINT ( 'NONE',  ( -1.202422216336444860, -0.2106116882872802742, 0.01209463403148830843 ) ) ;
#1641=LINE ( 'NONE', #1067, #4944 ) ;
#1642=CARTESIAN_POINT ( 'NONE',  ( 1.640223930642276118, 1.235377681956740803, -0.1039999999999998703 ) ) ;
#1647=AXIS2_PLACEMENT_3D ( 'NONE', #5744, #5211, #1386 ) ;
#1648=( CONVERSION_BASED_UNIT ( 'INCH', #345 ) LENGTH_UNIT ( ) NAMED_UNIT ( #3120 ) );
#1665=AXIS2_PLACEMENT_3D ( 'NONE', #156, #83, #3931 ) ;
#1668=EDGE_CURVE ( 'NONE', #3019, #7983, #4666, .T. ) ;
#1670=ORIENTED_EDGE ( 'NONE', *, *, #2725, .T. ) ;
#1671=CARTESIAN_POINT ( 'NONE',  ( -1.040997396242601791, -0.7528336330030669377, 0.03199999999999999373 ) ) ;
#1674=DIRECTION ( 'NONE',  ( -0.000000000000000000, -0.000000000000000000, -1.000000000000000000 ) ) ;
#1676=CARTESIAN_POINT ( 'NONE',  ( 1.620624198909131453, 1.220060950454640913, 0.1980431631100827705 ) ) ;
#1679=B_SPLINE_CURVE_WITH_KNOTS ( 'NONE', 3,
 ( #4396, #5045, #6888, #3159, #5662, #40, #7737, #862, #1426, #6430, #6318, #1962, #739, #7658 ),
 .UNSPECIFIED., .F., .F.,
 ( 4, 2, 2, 2, 2, 2, 4 ),
 ( 0.0003647048759916438976, 0.001831661078496667119, 0.003298617281001690448, 0.004032095382254203414, 0.004765573483506716813, 0.005499051584759229346, 0.006232529686011742745 ),
 .UNSPECIFIED. ) ;
#1682=CARTESIAN_POINT ( 'NONE',  ( 1.398758944919299640, 1.188821657285198841, 0.2500000000000000000 ) ) ;
#1695=CARTESIAN_POINT ( 'NONE',  ( -0.03921911030312481838, -0.4592703903598064352, 0.2500000000000000000 ) ) ;
#1703=FACE_OUTER_BOUND ( 'NONE', #2519, .T. ) ;
#1704=CARTESIAN_POINT ( 'NONE',  ( 1.478057046718104228, 1.237683112344551084, 0.2500000000000000555 ) ) ;
#1705=ORIENTED_EDGE ( 'NONE', *, *, #426, .T. ) ;
#1706=CARTESIAN_POINT ( 'NONE',  ( 1.537507892858355873, 1.215016084663213869, 0.1879675853768330851 ) ) ;
#1709=FACE_OUTER_BOUND ( 'NONE', #3841, .T. ) ;
#1710=CARTESIAN_POINT ( 'NONE',  ( 0.1028096983035132889, -0.4582465879184300372, 0.2500000000000000000 ) ) ;
#1713=ORIENTED_EDGE ( 'NONE', *, *, #5177, .F. ) ;
#1721=CARTESIAN_POINT ( 'NONE',  ( 0.9207653111462810180, 0.7459592875503607834, 0.2500000000000000000 ) ) ;
#1732=ORIENTED_EDGE ( 'NONE', *, *, #5123, .F. ) ;
#1733=CARTESIAN_POINT ( 'NONE',  ( 1.684866161243239846, 1.178252195112418299, -0.1039999999999998703 ) ) ;
#1734=CARTESIAN_POINT ( 'NONE',  ( 0.07619294758106566479, -0.4615701726917245673, 0.2315531569361643227 ) ) ;
#1739=EDGE_LOOP ( 'NONE', ( #3323, #1670, #7024, #7032, #5755 ) ) ;
#1740=CARTESIAN_POINT ( 'NONE',  ( 1.329175868372617808, 1.071828013948508573, -0.09195621454640677539 ) ) ;
#1741=CYLINDRICAL_SURFACE ( 'NONE', #7289, 3.939999999999463487 ) ;
#1743=CARTESIAN_POINT ( 'NONE',  ( 0.05830766503004893714, -0.4630768614767043490, 0.01347280640398593708 ) ) ;
#1748=CARTESIAN_POINT ( 'NONE',  ( 1.621822537759170402, 1.217706612625922613, 0.1978325958163386078 ) ) ;
#1749=DIRECTION ( 'NONE',  ( 0.000000000000000000, 0.000000000000000000, 1.000000000000000000 ) ) ;
#1752=FACE_OUTER_BOUND ( 'NONE', #923, .T. ) ;
#1760=DIRECTION ( 'NONE',  ( -0.7879377495398142139, -0.6157549048526800295, 0.000000000000000000 ) ) ;
#1763=ORIENTED_EDGE ( 'NONE', *, *, #884, .T. ) ;
#1785=CARTESIAN_POINT ( 'NONE',  ( 0.7938352818579558212, 1.310043527237274574, -0.3750000000000000555 ) ) ;
#1790=AXIS2_PLACEMENT_3D ( 'NONE', #1710, #5447, #604 ) ;
#1792=CARTESIAN_POINT ( 'NONE',  ( -6.110602001756019419, -1.404684638105634820, 0.000000000000000000 ) ) ;
#1797=ORIENTED_EDGE ( 'NONE', *, *, #7351, .F. ) ;
#1799=CARTESIAN_POINT ( 'NONE',  ( 1.293421091588340621, 1.088624948896591560, -0.1020512680642866737 ) ) ;
#1800=CARTESIAN_POINT ( 'NONE',  ( 1.515601125127084003, 1.045975532051838908, -0.1039999999999998287 ) ) ;
#1801=ORIENTED_EDGE ( 'NONE', *, *, #1275, .T. ) ;
#1802=ORIENTED_EDGE ( 'NONE', *, *, #1531, .F. ) ;
#1809=ORIENTED_EDGE ( 'NONE', *, *, #3992, .F. ) ;
#1818=ORIENTED_EDGE ( 'NONE', *, *, #272, .T. ) ;
#1821=CARTESIAN_POINT ( 'NONE',  ( 1.334235202004373511, 1.071904105284835262, -0.09796254303978589595 ) ) ;
#1824=CARTESIAN_POINT ( 'NONE',  ( 0.1028096983035134415, -0.4582465879184300372, 0.03199999999999999373 ) ) ;
#1830=ADVANCED_FACE ( 'NONE', ( #2275, #4212 ), #2934, .F. ) ;
#1840=FACE_BOUND ( 'NONE', #5319, .T. ) ;
#1844=ORIENTED_EDGE ( 'NONE', *, *, #7786, .T. ) ;
#1846=CARTESIAN_POINT ( 'NONE',  ( 1.537935346170436812, 1.852967428140057216, 0.000000000000000000 ) ) ;
#1847=ORIENTED_EDGE ( 'NONE', *, *, #5217, .T. ) ;
#1849=EDGE_LOOP ( 'NONE', ( #5180, #3452, #5025, #5421, #5082, #3393, #7960, #2688, #5587, #1763, #760, #2743 ) ) ;
#1861=CARTESIAN_POINT ( 'NONE',  ( 0.1014930221493801354, -0.4584436548183983828, 0.02922833221147581179 ) ) ;
#1864=CARTESIAN_POINT ( 'NONE',  ( 1.781235495941194680, 1.573674324865669938, -8.161306669393017495E-14 ) ) ;
#1871=CARTESIAN_POINT ( 'NONE',  ( 1.345270796830296378, 1.086053773142332757, -0.1449383704060485945 ) ) ;
#1872=ADVANCED_FACE ( 'NONE', ( #6105 ), #3621, .F. ) ;
#1874=CARTESIAN_POINT ( 'NONE',  ( -1.479329383613507964, -3.808562985511015242, 0.000000000000000000 ) ) ;
#1877=AXIS2_PLACEMENT_3D ( 'NONE', #854, #5860, #237 ) ;
#1885=DIRECTION ( 'NONE',  ( 0.000000000000000000, 0.000000000000000000, -1.000000000000000000 ) ) ;
#1890=CARTESIAN_POINT ( 'NONE',  ( -1.203304165734202735, -0.2076492422562720153, 0.2349865476952187893 ) ) ;
#1893=AXIS2_PLACEMENT_3D ( 'NONE', #5181, #7563, #55 ) ;
#1895=AXIS2_PLACEMENT_3D ( 'NONE', #6015, #6516, #1619 ) ;
#1897=ORIENTED_EDGE ( 'NONE', *, *, #374, .T. ) ;
#1902=CIRCLE ( 'NONE', #2016, 0.3750000000000000555 ) ;
#1903=CARTESIAN_POINT ( 'NONE',  ( 1.877707900143042563, 1.420965844381539167, -0.06059890939898970180 ) ) ;
#1904=AXIS2_PLACEMENT_3D ( 'NONE', #350, #261, #5361 ) ;
#1905=ORIENTED_EDGE ( 'NONE', *, *, #4342, .T. ) ;
#1907=( LENGTH_UNIT ( ) NAMED_UNIT ( * ) SI_UNIT ( $, .METRE. ) );
#1908=CARTESIAN_POINT ( 'NONE',  ( -1.750746777110393282, 1.631196835986985505, 0.3125000000000000000 ) ) ;
#1910=CARTESIAN_POINT ( 'NONE',  ( 0.9207653111462810180, 0.7459592875503607834, 0.2500000000000000000 ) ) ;
#1911=CARTESIAN_POINT ( 'NONE',  ( 1.674724282714340262, 1.670501082519673330, -0.02948104019479953763 ) ) ;
#1921=VERTEX_POINT ( 'NONE', #2666 ) ;
#1931=AXIS2_PLACEMENT_3D ( 'NONE', #7066, #5183, #5416 ) ;
#1936=EDGE_CURVE ( 'NONE', #2354, #3933, #4214, .T. ) ;
#1944=DIRECTION ( 'NONE',  ( 0.7879377495398141029, 0.6157549048526800295, 0.000000000000000000 ) ) ;
#1947=CARTESIAN_POINT ( 'NONE',  ( -0.5950975756886817125, 0.1840126700235228119, 0.2500000000000000000 ) ) ;
#1948=EDGE_LOOP ( 'NONE', ( #3768, #3454, #4859, #7832 ) ) ;
#1952=EDGE_LOOP ( 'NONE', ( #4874, #4730, #1224, #2728 ) ) ;
#1962=CARTESIAN_POINT ( 'NONE',  ( 1.258132545478801489, 1.077561972973184234, -0.07313160851655174655 ) ) ;
#1968=ORIENTED_EDGE ( 'NONE', *, *, #6931, .T. ) ;
#1973=DIRECTION ( 'NONE',  ( 0.7879377495398137699, 0.6157549048526805846, 0.000000000000000000 ) ) ;
#1976=DIRECTION ( 'NONE',  ( 0.8875604078987042733, -0.4606913525677314158, 0.000000000000000000 ) ) ;
#1979=( BOUNDED_SURFACE ( )  B_SPLINE_SURFACE ( 3, 2, ( 
 ( #1421, #3312, #2777 ),
 ( #4504, #3927, #4581 ),
 ( #5814, #912, #5249 ),
 ( #1510, #5288, #194 ),
 ( #2694, #5207, #7703 ),
 ( #2085, #7080, #3363 ),
 ( #7778, #3968, #5863 ),
 ( #241, #2738, #7732 ),
 ( #1556, #2123, #3405 ),
 ( #2172, #396, #5332 ) ),
 .UNSPECIFIED., .F., .F., .F. ) 
 B_SPLINE_SURFACE_WITH_KNOTS ( ( 4, 2, 2, 2, 4 ),
 ( 3, 3 ),
 ( 3.474043806539870438, 3.783630100001075025, 4.093216393462279612, 4.402802686923484643, 4.712388980384689674 ),
 ( 0.000000000000000000, 1.000000000000000000 ),
 .UNSPECIFIED. ) 
 GEOMETRIC_REPRESENTATION_ITEM ( )  RATIONAL_B_SPLINE_SURFACE ( (
 ( 1.000000000000000000, 0.7246887769596790374, 1.000000000000000000),
 ( 1.000000000000000000, 0.7240706762976710786, 1.000000000000000000),
 ( 1.000000000000000000, 0.7231708462380681546, 1.000000000000000000),
 ( 1.000000000000000000, 0.7208914930597065673, 1.000000000000000000),
 ( 1.000000000000000000, 0.7195114720895853244, 1.000000000000000000),
 ( 1.000000000000000000, 0.7163941252002704596, 1.000000000000000000),
 ( 1.000000000000000000, 0.7146571679537656596, 1.000000000000000000),
 ( 1.000000000000000000, 0.7109849263087011373, 1.000000000000000000),
 ( 1.000000000000000000, 0.7090503513044520423, 1.000000000000000000),
 ( 1.000000000000000000, 0.7071067811865479058, 1.000000000000000000) ) ) 
 REPRESENTATION_ITEM ( '' )  SURFACE ( )  );
#1980=AXIS2_PLACEMENT_3D ( 'NONE', #6410, #5179, #6297 ) ;
#1985=DIRECTION ( 'NONE',  ( 0.6157549048526803626, -0.7879377495398141029, 0.000000000000000000 ) ) ;
#1995=CARTESIAN_POINT ( 'NONE',  ( 1.848680164946085336, 1.461834501516724449, 0.02980581276967405810 ) ) ;
#2001=CARTESIAN_POINT ( 'NONE',  ( 1.800320205903117809, 1.030513867073702627, -0.1039999999999998703 ) ) ;
#2004=AXIS2_PLACEMENT_3D ( 'NONE', #966, #6617, #1007 ) ;
#2009=DIRECTION ( 'NONE',  ( -0.000000000000000000, -0.000000000000000000, -1.000000000000000000 ) ) ;
#2010=CIRCLE ( 'NONE', #2276, 0.1250000000000000000 ) ;
#2011=AXIS2_PLACEMENT_3D ( 'NONE', #3225, #1985, #4494 ) ;
#2012=CARTESIAN_POINT ( 'NONE',  ( 1.682670780591506876, 1.262878425707093744, 0.1946946326293004792 ) ) ;
#2016=AXIS2_PLACEMENT_3D ( 'NONE', #638, #7356, #3673 ) ;
#2019=ORIENTED_EDGE ( 'NONE', *, *, #5907, .F. ) ;
#2022=CARTESIAN_POINT ( 'NONE',  ( 0.1028096983035134415, -0.4582465879184300372, 0.2179999999999999993 ) ) ;
#2033=ADVANCED_FACE ( 'NONE', ( #4718 ), #7544, .T. ) ;
#2040=CIRCLE ( 'NONE', #6360, 0.3024878104020024550 ) ;
#2044=CARTESIAN_POINT ( 'NONE',  ( 1.860105863992942199, 1.471940519787515500, -0.01146616443475796492 ) ) ;
#2049=DIRECTION ( 'NONE',  ( 0.000000000000000000, 0.000000000000000000, -1.000000000000000000 ) ) ;
#2051=ORIENTED_EDGE ( 'NONE', *, *, #231, .T. ) ;
#2055=CIRCLE ( 'NONE', #361, 0.03199999999999997985 ) ;
#2057=AXIS2_PLACEMENT_3D ( 'NONE', #7401, #8078, #7357 ) ;
#2062=CARTESIAN_POINT ( 'NONE',  ( 1.753077028676194526, 1.307477063583168064, 0.1680974545641061857 ) ) ;
#2069=DIRECTION ( 'NONE',  ( 0.7879377495398139919, 0.6157549048526802515, 0.000000000000000000 ) ) ;
#2070=VERTEX_POINT ( 'NONE', #3497 ) ;
#2076=CARTESIAN_POINT ( 'NONE',  ( 1.706166322112642630, 1.356275593161428983, 0.2051386464529749154 ) ) ;
#2077=CARTESIAN_POINT ( 'NONE',  ( 1.393862768891835469, 1.061876785772673193, -0.1723397769375844824 ) ) ;
#2079=EDGE_CURVE ( 'NONE', #6908, #112, #5876, .T. ) ;
#2080=EDGE_CURVE ( 'NONE', #3032, #6429, #296, .T. ) ;
#2081=CARTESIAN_POINT ( 'NONE',  ( -9.251037553912103917, -0.6017136928027502218, -0.05999999999999999778 ) ) ;
#2082=B_SPLINE_CURVE_WITH_KNOTS ( 'NONE', 3,
 ( #2838, #7860, #293, #7097, #1602, #4763 ),
 .UNSPECIFIED., .F., .F.,
 ( 4, 2, 4 ),
 ( 6.316259036090116417E-16, 0.0006701634491691482601, 0.001340326898337664864 ),
 .UNSPECIFIED. ) ;
#2084=EDGE_CURVE ( 'NONE', #6859, #1218, #7265, .T. ) ;
#2085=CARTESIAN_POINT ( 'NONE',  ( 1.374642519223019832, 1.763930785958341962, 0.1748676107922683409 ) ) ;
#2091=CARTESIAN_POINT ( 'NONE',  ( 0.3373886113636296868, -0.3568617631054005757, 0.008742659207913911629 ) ) ;
#2094=DIRECTION ( 'NONE',  ( 0.7879377495398142139, 0.6157549048526801405, 0.000000000000000000 ) ) ;
#2099=CARTESIAN_POINT ( 'NONE',  ( 1.717580241504790273, 1.374761148290041257, 0.1672982580699149402 ) ) ;
#2100=ORIENTED_EDGE ( 'NONE', *, *, #1328, .F. ) ;
#2110=ORIENTED_EDGE ( 'NONE', *, *, #6048, .F. ) ;
#2111=VERTEX_POINT ( 'NONE', #5 ) ;
#2113=ORIENTED_EDGE ( 'NONE', *, *, #1579, .T. ) ;
#2114=CARTESIAN_POINT ( 'NONE',  ( 1.710641181630429219, 1.387640563648149250, 0.2051014882331889944 ) ) ;
#2117=VECTOR ( 'NONE', #3799, 39.37007874015748854 ) ;
#2119=CIRCLE ( 'NONE', #1208, 0.03200000000000003536 ) ;
#2120=B_SPLINE_CURVE_WITH_KNOTS ( 'NONE', 3,
 ( #7759, #417, #5388, #4724, #7194, #4116, #6618, #7224 ),
 .UNSPECIFIED., .F., .F.,
 ( 4, 2, 2, 4 ),
 ( 1.109483187648633347E-17, 0.0003176057502265475989, 0.0006352115004530840305, 0.001270423000906161989 ),
 .UNSPECIFIED. ) ;
#2123=CARTESIAN_POINT ( 'NONE',  ( 1.270760784386404385, 1.682749642158441361, 0.2498245760079802757 ) ) ;
#2124=DIRECTION ( 'NONE',  ( 1.000000000000000000, 0.000000000000000000, 0.000000000000000000 ) ) ;
#2134=EDGE_CURVE ( 'NONE', #4364, #6669, #6584, .T. ) ;
#2136=AXIS2_PLACEMENT_3D ( 'NONE', #8014, #4800, #3727 ) ;
#2140=ORIENTED_EDGE ( 'NONE', *, *, #2188, .F. ) ;
#2145=TOROIDAL_SURFACE ( 'NONE', #7513, 6.962657474112426748, 0.03200000000000000067 ) ;
#2146=CIRCLE ( 'NONE', #1099, 0.4070000000000002505 ) ;
#2147=FACE_OUTER_BOUND ( 'NONE', #7987, .T. ) ;
#2149=B_SPLINE_CURVE_WITH_KNOTS ( 'NONE', 3,
 ( #5084, #778, #3783, #3277, #1347, #4401 ),
 .UNSPECIFIED., .F., .F.,
 ( 4, 2, 4 ),
 ( 2.945200827377960913E-17, 0.001884585737150711168, 0.003769171474301399351 ),
 .UNSPECIFIED. ) ;
#2150=DIRECTION ( 'NONE',  ( -0.6157549048526801405, 0.7879377495398142139, 0.000000000000000000 ) ) ;
#2152=DIRECTION ( 'NONE',  ( -0.000000000000000000, -0.000000000000000000, 1.000000000000000000 ) ) ;
#2160=FACE_OUTER_BOUND ( 'NONE', #6951, .T. ) ;
#2161=ORIENTED_EDGE ( 'NONE', *, *, #5250, .T. ) ;
#2163=CARTESIAN_POINT ( 'NONE',  ( 1.451358053557619598, 1.823882180053259860, 0.1350113725148300858 ) ) ;
#2166=B_SPLINE_CURVE_WITH_KNOTS ( 'NONE', 3,
 ( #1195, #3704, #579, #6254, #3130, #3084, #5590, #5629, #3820, #6322, #5088, #1474 ),
 .UNSPECIFIED., .F., .F.,
 ( 4, 2, 2, 2, 2, 4 ),
 ( 2.684845590619915053E-17, 0.001673132518879472293, 0.003346265037758917697, 0.004182831297198636063, 0.005019397556638355296, 0.006692530075517771210 ),
 .UNSPECIFIED. ) ;
#2172=CARTESIAN_POINT ( 'NONE',  ( 1.240314151020239120, 1.658956310969642800, 0.2179999999999998883 ) ) ;
#2178=CARTESIAN_POINT ( 'NONE',  ( 1.387804320626534915, 1.063587717045087144, -0.1645371419711735006 ) ) ;
#2179=AXIS2_PLACEMENT_3D ( 'NONE', #2001, #4438, #703 ) ;
#2181=CARTESIAN_POINT ( 'NONE',  ( 1.516422131414766339, 1.874728233683303324, -0.007188475204957444839 ) ) ;
#2186=CARTESIAN_POINT ( 'NONE',  ( 1.517943318015056109, 1.875917005398948456, 0.03199999999999999373 ) ) ;
#2187=CARTESIAN_POINT ( 'NONE',  ( 1.517690421966769732, 1.264920623095007191, 0.2500000000000000000 ) ) ;
#2188=EDGE_CURVE ( 'NONE', #7797, #695, #1257, .T. ) ;
#2215=VERTEX_POINT ( 'NONE', #1194 ) ;
#2217=FACE_OUTER_BOUND ( 'NONE', #247, .T. ) ;
#2222=CARTESIAN_POINT ( 'NONE',  ( 1.142655413120957197, 0.6307864494084283180, 0.2500000000000000000 ) ) ;
#2228=CARTESIAN_POINT ( 'NONE',  ( 1.877707900143042563, 1.420965844381539167, -0.06059890939898970180 ) ) ;
#2229=CARTESIAN_POINT ( 'NONE',  ( 0.02199364308835362672, -0.4639489453757028592, 0.2441666941616341957 ) ) ;
#2232=VERTEX_POINT ( 'NONE', #3570 ) ;
#2237=DIRECTION ( 'NONE',  ( 0.7879377495398141029, 0.6157549048526802515, -0.000000000000000000 ) ) ;
#2246=DIRECTION ( 'NONE',  ( -1.000000000000000000, 0.000000000000000000, 0.000000000000000000 ) ) ;
#2249=( GEOMETRIC_REPRESENTATION_CONTEXT ( 3 ) GLOBAL_UNCERTAINTY_ASSIGNED_CONTEXT ( ( #3014 ) ) GLOBAL_UNIT_ASSIGNED_CONTEXT ( ( #1648, #5879, #4600 ) ) REPRESENTATION_CONTEXT ( 'NONE', 'WORKASPACE' ) );
#2255=ORIENTED_EDGE ( 'NONE', *, *, #2611, .F. ) ;
#2262=VERTEX_POINT ( 'NONE', #743 ) ;
#2263=DIRECTION ( 'NONE',  ( -1.000000000000000000, 0.000000000000000000, 0.000000000000000000 ) ) ;
#2264=DIRECTION ( 'NONE',  ( -1.000000000000000000, 0.000000000000000000, 0.000000000000000000 ) ) ;
#2265=FACE_OUTER_BOUND ( 'NONE', #7657, .T. ) ;
#2266=CIRCLE ( 'NONE', #1219, 0.03200000000000005618 ) ;
#2267=ORIENTED_EDGE ( 'NONE', *, *, #2429, .T. ) ;
#2269=CARTESIAN_POINT ( 'NONE',  ( 1.238969240134095040, 1.657905294597833201, 0.2179999999999999993 ) ) ;
#2274=ORIENTED_EDGE ( 'NONE', *, *, #6193, .F. ) ;
#2275=FACE_BOUND ( 'NONE', #7466, .T. ) ;
#2276=AXIS2_PLACEMENT_3D ( 'NONE', #109, #2640, #267 ) ;
#2281=ORIENTED_EDGE ( 'NONE', *, *, #6214, .T. ) ;
#2282=DIRECTION ( 'NONE',  ( -0.7879377495398141029, -0.6157549048526801405, 0.000000000000000000 ) ) ;
#2293=CARTESIAN_POINT ( 'NONE',  ( 0.1028096983035134415, -0.4582465879184300372, 0.2179999999999999993 ) ) ;
#2294=AXIS2_PLACEMENT_3D ( 'NONE', #5099, #6950, #3343 ) ;
#2299=DIRECTION ( 'NONE',  ( 1.000000000000000000, 0.000000000000000000, 0.000000000000000000 ) ) ;
#2302=ORIENTED_EDGE ( 'NONE', *, *, #3534, .F. ) ;
#2311=EDGE_LOOP ( 'NONE', ( #222, #5656, #5206, #6873 ) ) ;
#2312=EDGE_LOOP ( 'NONE', ( #4574, #6941, #4448, #7073 ) ) ;
#2320=CARTESIAN_POINT ( 'NONE',  ( 1.457966743008886068, 1.224466284236799041, 0.2500000000000000000 ) ) ;
#2322=ADVANCED_FACE ( 'NONE', ( #160 ), #7547, .F. ) ;
#2324=CARTESIAN_POINT ( 'NONE',  ( 1.496290583815347741, 1.216672708051755647, 0.2341988374537135043 ) ) ;
#2325=DIRECTION ( 'NONE',  ( 0.6157549048526801405, -0.7879377495398141029, 0.000000000000000000 ) ) ;
#2331=DIRECTION ( 'NONE',  ( 0.6157549048526804736, -0.7879377495398138809, -0.000000000000000000 ) ) ;
#2335=EDGE_CURVE ( 'NONE', #1300, #6, #3934, .T. ) ;
#2339=ORIENTED_EDGE ( 'NONE', *, *, #3925, .T. ) ;
#2340=DIRECTION ( 'NONE',  ( -0.000000000000000000, -0.000000000000000000, -1.000000000000000000 ) ) ;
#2341=DIRECTION ( 'NONE',  ( 0.000000000000000000, 0.000000000000000000, 1.000000000000000000 ) ) ;
#2345=CARTESIAN_POINT ( 'NONE',  ( 1.082008577330675347, 0.9412886604525910750, -0.3750000000000000555 ) ) ;
#2346=CARTESIAN_POINT ( 'NONE',  ( 0.05834656284656428160, -0.4630751787972929856, 0.2365186885590826738 ) ) ;
#2348=DIRECTION ( 'NONE',  ( -0.6157549048526801405, 0.7879377495398142139, 0.000000000000000000 ) ) ;
#2354=VERTEX_POINT ( 'NONE', #5163 ) ;
#2355=CARTESIAN_POINT ( 'NONE',  ( 1.568372102291784920, 1.166559938944232488, 0.1823255903230677766 ) ) ;
#2357=CARTESIAN_POINT ( 'NONE',  ( 1.278468178838435554, 1.054204894368677481, -0.03540237178041887034 ) ) ;
#2359=ORIENTED_EDGE ( 'NONE', *, *, #7480, .F. ) ;
#2360=CARTESIAN_POINT ( 'NONE',  ( 1.718286774861130795, 1.296381967182311135, 0.1842501703447952666 ) ) ;
#2368=CARTESIAN_POINT ( 'NONE',  ( 1.537918127343594454, 1.852987194258524983, 0.000000000000000000 ) ) ;
#2369=FACE_OUTER_BOUND ( 'NONE', #1174, .T. ) ;
#2372=EDGE_CURVE ( 'NONE', #225, #4105, #7664, .T. ) ;
#2373=CIRCLE ( 'NONE', #1980, 0.3045082206899650812 ) ;
#2376=VECTOR ( 'NONE', #4704, 39.37007874015748143 ) ;
#2383=EDGE_CURVE ( 'NONE', #3462, #2354, #2149, .T. ) ;
#2387=CARTESIAN_POINT ( 'NONE',  ( 0.3566525292043903339, -0.3408511508279103985, 0.2500000000000000000 ) ) ;
#2390=DIRECTION ( 'NONE',  ( -0.7540216022612866720, -0.6568496200222103676, 0.000000000000000000 ) ) ;
#2393=CARTESIAN_POINT ( 'NONE',  ( 1.558102590443268154, 1.816567841683527584, -0.02494716445955213677 ) ) ;
#2394=ORIENTED_EDGE ( 'NONE', *, *, #780, .T. ) ;
#2399=CARTESIAN_POINT ( 'NONE',  ( 0.1250000000000000000, 1.530808498934191509E-17, 0.2500000000000000000 ) ) ;
#2401=AXIS2_PLACEMENT_3D ( 'NONE', #4827, #2858, #7769 ) ;
#2402=EDGE_LOOP ( 'NONE', ( #3975, #3049, #1705, #5273, #3366, #7456 ) ) ;
#2405=AXIS2_PLACEMENT_3D ( 'NONE', #7856, #494, #6604 ) ;
#2407=CARTESIAN_POINT ( 'NONE',  ( 1.598412416413206305, 1.292942227395209365, 0.2367065158496169941 ) ) ;
#2409=ORIENTED_EDGE ( 'NONE', *, *, #1936, .F. ) ;
#2416=AXIS2_PLACEMENT_3D ( 'NONE', #4202, #3133, #1124 ) ;
#2429=EDGE_CURVE ( 'NONE', #4688, #2760, #4365, .T. ) ;
#2435=LINE ( 'NONE', #3756, #5857 ) ;
#2436=CARTESIAN_POINT ( 'NONE',  ( -0.02691317796861998624, -0.4609456947455670695, -2.734515813970577218E-17 ) ) ;
#2438=CYLINDRICAL_SURFACE ( 'NONE', #5169, 0.3099999999999745737 ) ;
#2448=AXIS2_PLACEMENT_3D ( 'NONE', #3759, #716, #2474 ) ;
#2449=LINE ( 'NONE', #6115, #3972 ) ;
#2451=ORIENTED_EDGE ( 'NONE', *, *, #4532, .T. ) ;
#2453=CARTESIAN_POINT ( 'NONE',  ( 1.733157827470031220, 1.373632878362992527, 0.1887011865795288901 ) ) ;
#2457=EDGE_CURVE ( 'NONE', #6908, #140, #5870, .T. ) ;
#2458=CARTESIAN_POINT ( 'NONE',  ( 0.9207653111462810180, 0.7459592875503607834, 0.03199999999999999373 ) ) ;
#2460=DIRECTION ( 'NONE',  ( -0.2853335501257686646, 0.9584282785752022971, 0.000000000000000000 ) ) ;
#2463=DIRECTION ( 'NONE',  ( 0.7879377495398138809, 0.6157549048526804736, 0.000000000000000000 ) ) ;
#2465=CARTESIAN_POINT ( 'NONE',  ( -0.6495791112554195612, -0.6379566159512914947, 0.2500000000000000000 ) ) ;
#2471=FACE_OUTER_BOUND ( 'NONE', #2476, .T. ) ;
#2472=CARTESIAN_POINT ( 'NONE',  ( 0.1009065958848031352, -0.4585303180291604996, 0.02870908699598821029 ) ) ;
#2474=DIRECTION ( 'NONE',  ( 0.2323175946639494671, -0.9726399823210830631, 0.000000000000000000 ) ) ;
#2475=CARTESIAN_POINT ( 'NONE',  ( 1.556400554713971651, 1.293514327272109687, 0.2500000000000000000 ) ) ;
#2476=EDGE_LOOP ( 'NONE', ( #623, #5473, #7791, #5235 ) ) ;
#2482=CARTESIAN_POINT ( 'NONE',  ( 1.340393471235059142, 1.071778002415290754, -0.1053413153387159629 ) ) ;
#2484=CARTESIAN_POINT ( 'NONE',  ( 1.790638542569023439, 1.445778985265036010, 0.1291092984545429978 ) ) ;
#2488=CARTESIAN_POINT ( 'NONE',  ( 1.723083782078303594, 1.395997476763640277, 0.1965221205737707477 ) ) ;
#2491=ORIENTED_EDGE ( 'NONE', *, *, #899, .F. ) ;
#2497=ORIENTED_EDGE ( 'NONE', *, *, #2080, .F. ) ;
#2500=CARTESIAN_POINT ( 'NONE',  ( 1.412217567875231783, 1.057196047309451492, -0.1989038500118037456 ) ) ;
#2502=CARTESIAN_POINT ( 'NONE',  ( -1.050138139902704104, -0.7221301030214424266, 0.2500000000000000000 ) ) ;
#2505=SHAPE_REPRESENTATION ( 'Cleco, Handle, Pivoting', ( #3555 ), #2249 ) ;
#2510=FACE_OUTER_BOUND ( 'NONE', #7662, .T. ) ;
#2519=EDGE_LOOP ( 'NONE', ( #7087, #1713, #5517, #7252 ) ) ;
#2522=CARTESIAN_POINT ( 'NONE',  ( 1.388552349919598194, 1.071937153724873859, -0.1822035261336616696 ) ) ;
#2523=CARTESIAN_POINT ( 'NONE',  ( 1.850068364776406682, 1.494658567734585608, 0.000000000000000000 ) ) ;
#2525=ORIENTED_EDGE ( 'NONE', *, *, #872, .T. ) ;
#2529=ORIENTED_EDGE ( 'NONE', *, *, #1569, .T. ) ;
#2535=DIRECTION ( 'NONE',  ( -0.000000000000000000, -0.000000000000000000, -1.000000000000000000 ) ) ;
#2536=LINE ( 'NONE', #859, #5584 ) ;
#2538=ORIENTED_EDGE ( 'NONE', *, *, #732, .F. ) ;
#2541=DIRECTION ( 'NONE',  ( 0.7879377495398137699, 0.6157549048526805846, 0.000000000000000000 ) ) ;
#2546=DIRECTION ( 'NONE',  ( -0.9726399823210830631, -0.2323175946639496336, 0.000000000000000000 ) ) ;
#2547=TOROIDAL_SURFACE ( 'NONE', #3336, 4.032000000000000917, 0.03200000000000000067 ) ;
#2549=CARTESIAN_POINT ( 'NONE',  ( -6.110602001756019419, -1.404684638105634820, -0.05999999999999999778 ) ) ;
#2550=AXIS2_PLACEMENT_3D ( 'NONE', #6333, #5843, #2069 ) ;
#2560=ORIENTED_EDGE ( 'NONE', *, *, #3480, .T. ) ;
#2563=PLANE ( 'NONE',  #843 ) ;
#2564=VERTEX_POINT ( 'NONE', #7742 ) ;
#2571=CIRCLE ( 'NONE', #611, 0.06249999999999995143 ) ;
#2577=DIRECTION ( 'NONE',  ( -0.6157549048526804736, 0.7879377495398138809, 0.000000000000000000 ) ) ;
#2579=ORIENTED_EDGE ( 'NONE', *, *, #1581, .F. ) ;
#2584=CARTESIAN_POINT ( 'NONE',  ( -5.996547682996108186, -1.882193845889703843, 0.000000000000000000 ) ) ;
#2587=EDGE_CURVE ( 'NONE', #577, #7415, #2726, .T. ) ;
#2594=FACE_OUTER_BOUND ( 'NONE', #6978, .T. ) ;
#2598=ORIENTED_EDGE ( 'NONE', *, *, #1579, .F. ) ;
#2600=DIRECTION ( 'NONE',  ( -0.000000000000000000, -0.000000000000000000, -1.000000000000000000 ) ) ;
#2603=CARTESIAN_POINT ( 'NONE',  ( 1.833071640066518793, 1.461597232314661099, 0.07336022493874648498 ) ) ;
#2608=DIRECTION ( 'NONE',  ( 0.7879377495398124376, 0.6157549048526823610, -0.000000000000000000 ) ) ;
#2609=ORIENTED_EDGE ( 'NONE', *, *, #3349, .F. ) ;
#2610=CARTESIAN_POINT ( 'NONE',  ( -0.1250000000000000000, 0.000000000000000000, 0.2500000000000000000 ) ) ;
#2611=EDGE_CURVE ( 'NONE', #7825, #3263, #7458, .T. ) ;
#2615=DIRECTION ( 'NONE',  ( 0.6157549048526803626, -0.7879377495398141029, 0.000000000000000000 ) ) ;
#2616=ADVANCED_FACE ( 'NONE', ( #4305 ), #6674, .T. ) ;
#2618=CARTESIAN_POINT ( 'NONE',  ( 1.240314151020239564, 1.658956310969643022, 0.2179999999999999993 ) ) ;
#2622=ORIENTED_EDGE ( 'NONE', *, *, #5635, .F. ) ;
#2623=ORIENTED_EDGE ( 'NONE', *, *, #2457, .T. ) ;
#2625=ADVANCED_FACE ( 'NONE', ( #1840, #5526 ), #6801, .T. ) ;
#2627=B_SPLINE_CURVE_WITH_KNOTS ( 'NONE', 3,
 ( #606, #5691, #70, #4461, #2484, #1217, #7001, #3725, #3808, #2523 ),
 .UNSPECIFIED., .F., .F.,
 ( 4, 2, 2, 2, 4 ),
 ( 1.944054687082719846E-15, 0.001638661185932331404, 0.003277322371862718617, 0.004915983557793104745, 0.006554644743723490874 ),
 .UNSPECIFIED. ) ;
#2628=DIRECTION ( 'NONE',  ( 0.7879377495398141029, 0.6157549048526801405, 0.000000000000000000 ) ) ;
#2630=CARTESIAN_POINT ( 'NONE',  ( 1.594233409951963720, 1.779210072867621673, -0.05526284733805063992 ) ) ;
#2631=CARTESIAN_POINT ( 'NONE',  ( -1.275477614966805673, 0.03477957369036089458, 0.000000000000000000 ) ) ;
#2635=ORIENTED_EDGE ( 'NONE', *, *, #3873, .F. ) ;
#2637=DIRECTION ( 'NONE',  ( 0.7879377495398138809, 0.6157549048526802515, 0.000000000000000000 ) ) ;
#2640=DIRECTION ( 'NONE',  ( 0.000000000000000000, 0.000000000000000000, 1.000000000000000000 ) ) ;
#2648=CARTESIAN_POINT ( 'NONE',  ( 1.814546527701561329, 1.464390739155001953, 0.09167169929298568665 ) ) ;
#2652=AXIS2_PLACEMENT_3D ( 'NONE', #2081, #7172, #1554 ) ;
#2653=LINE ( 'NONE', #5159, #7284 ) ;
#2654=CARTESIAN_POINT ( 'NONE',  ( -1.199609308151822873, -0.2200601767247205021, 0.2460795971987651820 ) ) ;
#2655=EDGE_LOOP ( 'NONE', ( #6409, #352, #1306, #2560, #5999, #2451 ) ) ;
#2664=CARTESIAN_POINT ( 'NONE',  ( 0.2976660692273690456, -0.3850326757561704505, 0.2500000000000000000 ) ) ;
#2666=CARTESIAN_POINT ( 'NONE',  ( -1.194903880989551359, -0.2358655892081394090, 0.000000000000000000 ) ) ;
#2679=EDGE_CURVE ( 'NONE', #3298, #2215, #2449, .T. ) ;
#2685=CARTESIAN_POINT ( 'NONE',  ( 1.623596292979297528, 1.309516105093665228, 0.2332408580811136944 ) ) ;
#2688=ORIENTED_EDGE ( 'NONE', *, *, #5123, .T. ) ;
#2690=VECTOR ( 'NONE', #7615, 39.37007874015748143 ) ;
#2692=CIRCLE ( 'NONE', #2836, 0.03200000000000003536 ) ;
#2694=CARTESIAN_POINT ( 'NONE',  ( 1.420131823442061014, 1.799479612255304284, 0.1337826180019923150 ) ) ;
#2698=VERTEX_POINT ( 'NONE', #7332 ) ;
#2705=FACE_OUTER_BOUND ( 'NONE', #7695, .T. ) ;
#2710=DIRECTION ( 'NONE',  ( -0.000000000000000000, -0.000000000000000000, 1.000000000000000000 ) ) ;
#2716=CARTESIAN_POINT ( 'NONE',  ( -0.6495791112554195612, -0.6379566159512914947, 0.03199999999999999373 ) ) ;
#2721=ORIENTED_EDGE ( 'NONE', *, *, #4533, .T. ) ;
#2725=EDGE_CURVE ( 'NONE', #2564, #6669, #1354, .T. ) ;
#2726=B_SPLINE_CURVE_WITH_KNOTS ( 'NONE', 3,
 ( #6533, #918, #7783, #2178, #4676, #3444 ),
 .UNSPECIFIED., .F., .F.,
 ( 4, 2, 4 ),
 ( 0.002381428155045459648, 0.003857366089970378029, 0.005333304024895296411 ),
 .UNSPECIFIED. ) ;
#2728=ORIENTED_EDGE ( 'NONE', *, *, #5354, .F. ) ;
#2730=ORIENTED_EDGE ( 'NONE', *, *, #7399, .T. ) ;
#2731=CARTESIAN_POINT ( 'NONE',  ( 1.678550149446894624, 1.340866106857560247, 0.2177700924245533909 ) ) ;
#2734=ORIENTED_EDGE ( 'NONE', *, *, #5540, .T. ) ;
#2738=CARTESIAN_POINT ( 'NONE',  ( 1.301246111754461809, 1.706573211805008539, 0.2436449323019636015 ) ) ;
#2743=ORIENTED_EDGE ( 'NONE', *, *, #882, .F. ) ;
#2751=DIRECTION ( 'NONE',  ( 0.6157549048526804736, -0.7879377495398138809, -0.000000000000000000 ) ) ;
#2755=CYLINDRICAL_SURFACE ( 'NONE', #753, 7.490657474112464520 ) ;
#2758=CYLINDRICAL_SURFACE ( 'NONE', #1904, 0.3024878104022636904 ) ;
#2760=VERTEX_POINT ( 'NONE', #5655 ) ;
#2767=CARTESIAN_POINT ( 'NONE',  ( 1.620241226944308055, 1.319147010849713419, 0.2447046302806205054 ) ) ;
#2772=DIRECTION ( 'NONE',  ( -0.7879377495398141029, -0.6157549048526800295, -0.000000000000000000 ) ) ;
#2775=AXIS2_PLACEMENT_3D ( 'NONE', #1299, #3266, #5076 ) ;
#2777=CARTESIAN_POINT ( 'NONE',  ( 1.538653472941177380, 1.853533897300119637, -0.002614644835676915424 ) ) ;
#2782=DIRECTION ( 'NONE',  ( 0.6157549048526803626, -0.7879377495398141029, 0.000000000000000000 ) ) ;
#2798=CARTESIAN_POINT ( 'NONE',  ( 1.640223930642815242, 1.235377681955144746, -0.1039999999999998703 ) ) ;
#2799=CARTESIAN_POINT ( 'NONE',  ( 1.552534361087756443, 1.258070674485461060, 0.2367071595535535922 ) ) ;
#2803=AXIS2_PLACEMENT_3D ( 'NONE', #1290, #3015, #2390 ) ;
#2806=CIRCLE ( 'NONE', #2011, 0.2148203157102362704 ) ;
#2810=ORIENTED_EDGE ( 'NONE', *, *, #7595, .F. ) ;
#2815=VERTEX_POINT ( 'NONE', #4477 ) ;
#2819=AXIS2_PLACEMENT_3D ( 'NONE', #7976, #7375, #4805 ) ;
#2821=DIRECTION ( 'NONE',  ( 0.7879377495398141029, 0.6157549048526802515, 6.186071356164057065E-15 ) ) ;
#2825=DIRECTION ( 'NONE',  ( 0.000000000000000000, 0.000000000000000000, 1.000000000000000000 ) ) ;
#2829=( BOUNDED_SURFACE ( )  B_SPLINE_SURFACE ( 3, 2, ( 
 ( #4161, #6546, #6010 ),
 ( #1044, #4077, #2880 ),
 ( #7866, #967, #4199 ),
 ( #6040, #3421, #3387 ) ),
 .UNSPECIFIED., .F., .F., .T. ) 
 B_SPLINE_SURFACE_WITH_KNOTS ( ( 4, 4 ),
 ( 3, 3 ),
 ( 2.890916672715349023E-15, 0.001713611390987410501 ),
 ( 0.000000000000000000, 1.000000000000000000 ),
 .UNSPECIFIED. ) 
 GEOMETRIC_REPRESENTATION_ITEM ( )  RATIONAL_B_SPLINE_SURFACE ( (
 ( 1.000000000000000000, 0.7881701093123700819, 1.000000000000000000),
 ( 1.000000000000000000, 0.7634790912858369083, 1.000000000000000000),
 ( 1.000000000000000000, 0.7360895404014861088, 1.000000000000000000),
 ( 1.000000000000000000, 0.7071067811865471286, 1.000000000000000000) ) ) 
 REPRESENTATION_ITEM ( '' )  SURFACE ( )  );
#2833=CARTESIAN_POINT ( 'NONE',  ( 1.417678740269246340, 1.200983045140381122, 0.2500000000000000000 ) ) ;
#2836=AXIS2_PLACEMENT_3D ( 'NONE', #7818, #4625, #7130 ) ;
#2837=AXIS2_PLACEMENT_3D ( 'NONE', #5291, #2782, #7780 ) ;
#2838=CARTESIAN_POINT ( 'NONE',  ( 1.492904096916551460, 1.856349440303736831, -0.001813861035895662039 ) ) ;
#2841=ADVANCED_FACE ( 'NONE', ( #5077 ), #730, .T. ) ;
#2843=ORIENTED_EDGE ( 'NONE', *, *, #7592, .F. ) ;
#2846=SHAPE_REPRESENTATION_RELATIONSHIP ( 'NONE' , 'NONE' ,  #2505, #3861 ) ;
#2849=CARTESIAN_POINT ( 'NONE',  ( -0.01467241879803482009, -0.4621469832361911889, 0.2490901869219590559 ) ) ;
#2857=DESIGN_CONTEXT ( 'detailed design', #7659, 'design' ) ;
#2858=DIRECTION ( 'NONE',  ( -0.6157549048526804736, 0.7879377495398138809, 0.000000000000000000 ) ) ;
#2862=CARTESIAN_POINT ( 'NONE',  ( -1.194903880989551359, -0.2358655892081394090, 0.2500000000000000000 ) ) ;
#2869=CARTESIAN_POINT ( 'NONE',  ( -1.204376266962890796, -0.2040480809676099294, 0.02769383754956057653 ) ) ;
#2870=CARTESIAN_POINT ( 'NONE',  ( 1.515234606834908515, 1.873800211025280271, -0.03184469952871944037 ) ) ;
#2873=DIRECTION ( 'NONE',  ( -0.7879377495398137699, -0.6157549048526804736, 9.031266384036010773E-16 ) ) ;
#2880=CARTESIAN_POINT ( 'NONE',  ( 1.434403980295607450, 1.174077354389669425, 0.2232676372131965070 ) ) ;
#2882=CARTESIAN_POINT ( 'NONE',  ( 0.09537553527426689826, -0.4271221084841553828, 0.03199999999999999373 ) ) ;
#2889=CARTESIAN_POINT ( 'NONE',  ( -0.5950975756886838219, 0.1840126700235215629, 0.000000000000000000 ) ) ;
#2896=DIRECTION ( 'NONE',  ( -0.000000000000000000, -0.000000000000000000, -1.000000000000000000 ) ) ;
#2916=ORIENTED_EDGE ( 'NONE', *, *, #528, .F. ) ;
#2922=CIRCLE ( 'NONE', #3582, 0.2704878104020023710 ) ;
#2924=CIRCLE ( 'NONE', #7512, 0.03200000000000009781 ) ;
#2932=CARTESIAN_POINT ( 'NONE',  ( 1.437142212823555587, 1.212327995211809117, 0.2500000000000000000 ) ) ;
#2933=ORIENTED_EDGE ( 'NONE', *, *, #5738, .F. ) ;
#2934=PLANE ( 'NONE',  #550 ) ;
#2938=FACE_OUTER_BOUND ( 'NONE', #653, .T. ) ;
#2939=ADVANCED_FACE ( 'NONE', ( #6590 ), #7774, .T. ) ;
#2940=ORIENTED_EDGE ( 'NONE', *, *, #899, .T. ) ;
#2949=VECTOR ( 'NONE', #5800, 39.37007874015748143 ) ;
#2950=AXIS2_PLACEMENT_3D ( 'NONE', #4216, #2985, #6715 ) ;
#2952=CARTESIAN_POINT ( 'NONE',  ( 1.537977733798261415, 1.853045334091375951, 0.0002768784213065589631 ) ) ;
#2959=EDGE_LOOP ( 'NONE', ( #6461, #7561, #1182, #7198 ) ) ;
#2960=CIRCLE ( 'NONE', #3221, 0.3243589946935201418 ) ;
#2961=CARTESIAN_POINT ( 'NONE',  ( 1.708525763102507256, 1.357565861344007141, 0.2042212951862970305 ) ) ;
#2965=ORIENTED_EDGE ( 'NONE', *, *, #2679, .F. ) ;
#2967=CARTESIAN_POINT ( 'NONE',  ( 0.1024609768753887706, -0.4582992960660679516, 0.2195113138857777701 ) ) ;
#2969=DIRECTION ( 'NONE',  ( -0.6930146854838814541, -0.5415747525370658844, -0.4758439167606253739 ) ) ;
#2973=CARTESIAN_POINT ( 'NONE',  ( 1.318949359038512847, 1.070937463555512004, -0.08001666686726011113 ) ) ;
#2979=AXIS2_PLACEMENT_3D ( 'NONE', #136, #175, #2628 ) ;
#2980=DIRECTION ( 'NONE',  ( 0.000000000000000000, 0.000000000000000000, 1.000000000000000000 ) ) ;
#2982=EDGE_CURVE ( 'NONE', #5415, #4005, #2266, .T. ) ;
#2983=CARTESIAN_POINT ( 'NONE',  ( 1.534341089483872489, 1.136888306601122611, 0.1623010253712050266 ) ) ;
#2985=DIRECTION ( 'NONE',  ( 0.000000000000000000, 0.000000000000000000, 1.000000000000000000 ) ) ;
#2987=CARTESIAN_POINT ( 'NONE',  ( 1.264570944868384839, 1.043344531369262862, -0.06210292240206113229 ) ) ;
#2989=EDGE_CURVE ( 'NONE', #7979, #6859, #4368, .T. ) ;
#2995=EDGE_CURVE ( 'NONE', #3183, #6242, #2922, .T. ) ;
#3005=B_SPLINE_CURVE_WITH_KNOTS ( 'NONE', 3,
 ( #4758, #2869, #995, #7256, #1636, #4223, #450, #5412, #4146, #6644 ),
 .UNSPECIFIED., .F., .F.,
 ( 4, 2, 2, 2, 4 ),
 ( 0.000000000000000000, 0.0003233994580137520723, 0.0006467989160275039277, 0.0009701983740412558916, 0.001293597832055007639 ),
 .UNSPECIFIED. ) ;
#3011=CARTESIAN_POINT ( 'NONE',  ( -1.040997396242602013, -0.7528336330030671597, 0.2222280897328365867 ) ) ;
#3014=UNCERTAINTY_MEASURE_WITH_UNIT (LENGTH_MEASURE( 1.000000000000000082E-05 ), #1648, 'distance_accuracy_value', 'NONE');
#3015=DIRECTION ( 'NONE',  ( -0.6568496200222103676, 0.7540216022612867830, 0.000000000000000000 ) ) ;
#3018=CARTESIAN_POINT ( 'NONE',  ( -0.6495791112554195612, -0.6379566159512914947, 0.2179999999999999993 ) ) ;
#3019=VERTEX_POINT ( 'NONE', #2862 ) ;
#3020=CARTESIAN_POINT ( 'NONE',  ( 1.570659431541528983, 1.272357891351626913, 0.2374606253409364820 ) ) ;
#3022=DIRECTION ( 'NONE',  ( 0.000000000000000000, 0.000000000000000000, -1.000000000000000000 ) ) ;
#3023=CARTESIAN_POINT ( 'NONE',  ( 1.316905486937928416, 1.070699082457407636, -0.07765199519505219805 ) ) ;
#3025=ORIENTED_EDGE ( 'NONE', *, *, #6995, .T. ) ;
#3030=DIRECTION ( 'NONE',  ( -1.000000000000000000, 0.000000000000000000, 0.000000000000000000 ) ) ;
#3032=VERTEX_POINT ( 'NONE', #5245 ) ;
#3033=DIRECTION ( 'NONE',  ( 1.000000000000000000, -9.460047923712866088E-16, 0.000000000000000000 ) ) ;
#3034=CARTESIAN_POINT ( 'NONE',  ( 0.2796912674003787513, -4.528516545235624413, 0.2500000000000000000 ) ) ;
#3038=EDGE_CURVE ( 'NONE', #1048, #7187, #4705, .T. ) ;
#3041=VERTEX_POINT ( 'NONE', #3473 ) ;
#3042=LINE ( 'NONE', #6130, #6982 ) ;
#3048=AXIS2_PLACEMENT_3D ( 'NONE', #42, #3203, #2541 ) ;
#3049=ORIENTED_EDGE ( 'NONE', *, *, #3534, .T. ) ;
#3050=LINE ( 'NONE', #3712, #7524 ) ;
#3056=CARTESIAN_POINT ( 'NONE',  ( 1.587288320519282703, 1.780102713094158018, -0.02630007929079021534 ) ) ;
#3059=VECTOR ( 'NONE', #1240, 39.37007874015748854 ) ;
#3062=CARTESIAN_POINT ( 'NONE',  ( 1.244866787913109674, 1.068558539354471204, -0.06210292240210990578 ) ) ;
#3064=TOROIDAL_SURFACE ( 'NONE', #1353, 0.2468203157102362433, 0.03200000000000000067 ) ;
#3071=CARTESIAN_POINT ( 'NONE',  ( 1.733157827467803669, 1.373632878365994348, 0.1887011865793609411 ) ) ;
#3075=CARTESIAN_POINT ( 'NONE',  ( 1.283086085828156087, 1.692381576688154032, -0.1039999999999998703 ) ) ;
#3076=CARTESIAN_POINT ( 'NONE',  ( 1.780616048947831098, 1.055727875058976251, -0.08212881570848259982 ) ) ;
#3079=EDGE_LOOP ( 'NONE', ( #7013, #7033, #5944, #1564 ) ) ;
#3081=EDGE_CURVE ( 'NONE', #3933, #3711, #5899, .T. ) ;
#3082=ADVANCED_FACE ( 'NONE', ( #2938 ), #2145, .T. ) ;
#3083=ADVANCED_FACE ( 'NONE', ( #4297 ), #3322, .T. ) ;
#3084=CARTESIAN_POINT ( 'NONE',  ( 1.806645078677039162, 1.428345690121396894, 0.1127449327592511957 ) ) ;
#3091=AXIS2_PLACEMENT_3D ( 'NONE', #3034, #6680, #7426 ) ;
#3092=ADVANCED_FACE ( 'NONE', ( #6107 ), #1172, .F. ) ;
#3098=AXIS2_PLACEMENT_3D ( 'NONE', #5707, #3932, #84 ) ;
#3104=CARTESIAN_POINT ( 'NONE',  ( 1.589183446880458206, 1.785275342778416929, -0.05425644835043919034 ) ) ;
#3113=CARTESIAN_POINT ( 'NONE',  ( 1.323123159461853326, 1.089031584755306259, -0.1264980700302772432 ) ) ;
#3120=DIMENSIONAL_EXPONENTS ( 1.000000000000000000, 0.000000000000000000, 0.000000000000000000, 0.000000000000000000, 0.000000000000000000, 0.000000000000000000, 0.000000000000000000 ) ;
#3130=CARTESIAN_POINT ( 'NONE',  ( 1.822942581281881136, 1.440962976019389608, 0.08718017679867827441 ) ) ;
#3133=DIRECTION ( 'NONE',  ( -0.7879377495398141029, -0.6157549048526802515, 0.000000000000000000 ) ) ;
#3135=ORIENTED_EDGE ( 'NONE', *, *, #1538, .F. ) ;
#3136=CARTESIAN_POINT ( 'NONE',  ( 1.339249842318065653, 1.071711091725345621, -0.1040000000000607383 ) ) ;
#3142=DIRECTION ( 'NONE',  ( -0.4606913525677331367, -0.8875604078987033851, 0.000000000000000000 ) ) ;
#3143=CARTESIAN_POINT ( 'NONE',  ( 1.820728631330852609, 1.486631279361974478, -0.03246653637537286891 ) ) ;
#3158=ORIENTED_EDGE ( 'NONE', *, *, #123, .T. ) ;
#3159=CARTESIAN_POINT ( 'NONE',  ( 1.360211532822002800, 1.082033417235804373, -0.1575618645360782888 ) ) ;
#3161=EDGE_LOOP ( 'NONE', ( #1327, #2940, #7959, #1591, #6867, #7613, #5130, #3559 ) ) ;
#3165=FACE_OUTER_BOUND ( 'NONE', #6805, .T. ) ;
#3166=CARTESIAN_POINT ( 'NONE',  ( 1.780616048947831986, 1.055727875058976917, -0.1039999999999998703 ) ) ;
#3168=CARTESIAN_POINT ( 'NONE',  ( 1.554085806680376436, 0.9967294227056006095, -0.1039999999999998287 ) ) ;
#3169=AXIS2_PLACEMENT_3D ( 'NONE', #4265, #3652, #6149 ) ;
#3172=DIRECTION ( 'NONE',  ( -0.000000000000000000, -0.000000000000000000, -1.000000000000000000 ) ) ;
#3176=DIRECTION ( 'NONE',  ( 0.000000000000000000, 0.000000000000000000, 1.000000000000000000 ) ) ;
#3177=CARTESIAN_POINT ( 'NONE',  ( 1.800320205903116921, 1.030513867073702183, -0.08212881570848259982 ) ) ;
#3178=VECTOR ( 'NONE', #1309, 39.37007874015748143 ) ;
#3179=EDGE_CURVE ( 'NONE', #5222, #5561, #5420, .T. ) ;
#3183=VERTEX_POINT ( 'NONE', #1021 ) ;
#3189=CARTESIAN_POINT ( 'NONE',  ( -0.6148017326439689789, 0.2092266780087954636, 0.03199999999999999373 ) ) ;
#3193=CIRCLE ( 'NONE', #8025, 0.3243589946935201418 ) ;
#3197=DIRECTION ( 'NONE',  ( -0.6157549048526801405, 0.7879377495398142139, 0.000000000000000000 ) ) ;
#3203=DIRECTION ( 'NONE',  ( 0.6157549048526804736, -0.7879377495398138809, -0.000000000000000000 ) ) ;
#3205=AXIS2_PLACEMENT_3D ( 'NONE', #7768, #7166, #1548 ) ;
#3215=AXIS2_PLACEMENT_3D ( 'NONE', #6419, #6343, #800 ) ;
#3217=DIRECTION ( 'NONE',  ( -0.9584282785752022971, -0.2853335501257686646, 0.000000000000000000 ) ) ;
#3221=AXIS2_PLACEMENT_3D ( 'NONE', #3866, #169, #7557 ) ;
#3222=VERTEX_POINT ( 'NONE', #2716 ) ;
#3225=CARTESIAN_POINT ( 'NONE',  ( 1.780616048947831986, 1.055727875058976917, -0.1039999999999998703 ) ) ;
#3228=CARTESIAN_POINT ( 'NONE',  ( 1.718386282410942600, 1.375744605918879593, 0.2061739259319994577 ) ) ;
#3235=CARTESIAN_POINT ( 'NONE',  ( 1.773383007244042631, 1.432796503982046943, 0.1500871045907652412 ) ) ;
#3238=ADVANCED_FACE ( 'NONE', ( #2147 ), #306, .T. ) ;
#3239=VERTEX_POINT ( 'NONE', #3999 ) ;
#3240=ADVANCED_FACE ( 'NONE', ( #4076 ), #4601, .F. ) ;
#3242=CARTESIAN_POINT ( 'NONE',  ( -1.196132095472828727, -0.2317400473908176328, 0.2500000000000001110 ) ) ;
#3243=ORIENTED_EDGE ( 'NONE', *, *, #3394, .T. ) ;
#3251=CARTESIAN_POINT ( 'NONE',  ( 1.713744337812789009, 1.365763491892051373, 0.1712939242540917617 ) ) ;
#3255=CARTESIAN_POINT ( 'NONE',  ( -0.6148017326439689789, 0.2092266780087954636, 0.2179999999999999993 ) ) ;
#3257=FACE_OUTER_BOUND ( 'NONE', #7113, .T. ) ;
#3263=VERTEX_POINT ( 'NONE', #3386 ) ;
#3266=DIRECTION ( 'NONE',  ( 0.4606913525677331367, 0.8875604078987033851, 0.000000000000000000 ) ) ;
#3270=CARTESIAN_POINT ( 'NONE',  ( 1.781945410564037768, 1.422047848568809059, 0.1506494843211809709 ) ) ;
#3271=CARTESIAN_POINT ( 'NONE',  ( -0.03921911030312481838, -0.4592703903598064352, 0.2500000000000000000 ) ) ;
#3277=CARTESIAN_POINT ( 'NONE',  ( 1.493295815665055759, 1.213146689595488326, 0.2319700209806794811 ) ) ;
#3289=B_SPLINE_CURVE_WITH_KNOTS ( 'NONE', 3,
 ( #4693, #4079, #302, #4657, #4003, #3507 ),
 .UNSPECIFIED., .F., .F.,
 ( 4, 2, 4 ),
 ( 1.256969020782943308E-21, 0.0003533183248413553470, 0.0007066366496827106939 ),
 .UNSPECIFIED. ) ;
#3292=ORIENTED_EDGE ( 'NONE', *, *, #4342, .F. ) ;
#3293=CARTESIAN_POINT ( 'NONE',  ( 1.684866161243239846, 1.178252195112418299, -0.1039999999999998703 ) ) ;
#3295=CYLINDRICAL_SURFACE ( 'NONE', #7296, 0.03199999999999986189 ) ;
#3296=CARTESIAN_POINT ( 'NONE',  ( -1.040997396242601791, -0.7528336330030669377, 0.2500000000000000000 ) ) ;
#3298=VERTEX_POINT ( 'NONE', #5964 ) ;
#3302=ORIENTED_EDGE ( 'NONE', *, *, #7300, .F. ) ;
#3304=ORIENTED_EDGE ( 'NONE', *, *, #4050, .T. ) ;
#3305=CIRCLE ( 'NONE', #954, 0.03199999999999997985 ) ;
#3306=CARTESIAN_POINT ( 'NONE',  ( 1.612360986893233372, 1.332289325118119150, 0.2442303131640376490 ) ) ;
#3307=CARTESIAN_POINT ( 'NONE',  ( 1.358097358395378151, 1.070245242547174680, -0.1269261509454146786 ) ) ;
#3312=CARTESIAN_POINT ( 'NONE',  ( 1.518800558058658989, 1.876586918424175465, -0.003115248787935155639 ) ) ;
#3313=DIRECTION ( 'NONE',  ( -0.7879377495398138809, -0.6157549048526803626, 0.000000000000000000 ) ) ;
#3317=CARTESIAN_POINT ( 'NONE',  ( 1.411244833761398310, 1.056435878372752324, -0.1949596646313069837 ) ) ;
#3322=TOROIDAL_SURFACE ( 'NONE', #7374, 0.2923589946935198913, 0.03200000000000000067 ) ;
#3323=ORIENTED_EDGE ( 'NONE', *, *, #576, .T. ) ;
#3329=ADVANCED_FACE ( 'NONE', ( #299 ), #5315, .T. ) ;
#3332=VECTOR ( 'NONE', #2237, 39.37007874015747433 ) ;
#3336=AXIS2_PLACEMENT_3D ( 'NONE', #8038, #1245, #7400 ) ;
#3338=EDGE_CURVE ( 'NONE', #6611, #3346, #5565, .T. ) ;
#3342=LINE ( 'NONE', #4809, #6126 ) ;
#3343=DIRECTION ( 'NONE',  ( -1.000000000000000000, 0.000000000000000000, 0.000000000000000000 ) ) ;
#3346=VERTEX_POINT ( 'NONE', #6853 ) ;
#3347=CIRCLE ( 'NONE', #2819, 0.3024878104020024550 ) ;
#3349=EDGE_CURVE ( 'NONE', #1006, #445, #1160, .T. ) ;
#3353=AXIS2_PLACEMENT_3D ( 'NONE', #508, #2969, #7471 ) ;
#3355=CARTESIAN_POINT ( 'NONE',  ( 1.717034119172104800, 1.391647134812390663, 0.2009755516559021404 ) ) ;
#3359=CIRCLE ( 'NONE', #4271, 0.3099999999999745737 ) ;
#3363=CARTESIAN_POINT ( 'NONE',  ( 1.406322310917426543, 1.749149093313088876, 0.2028435978050005528 ) ) ;
#3366=ORIENTED_EDGE ( 'NONE', *, *, #7629, .T. ) ;
#3368=CARTESIAN_POINT ( 'NONE',  ( 0.3553155032461795537, -0.3420189219808928982, 0.02497744489995550390 ) ) ;
#3374=DIRECTION ( 'NONE',  ( 0.6157549048526801405, -0.7879377495398141029, -0.000000000000000000 ) ) ;
#3379=CARTESIAN_POINT ( 'NONE',  ( 0.3517571870377138588, -0.3450675717666435438, 0.2305015624669528862 ) ) ;
#3380=CARTESIAN_POINT ( 'NONE',  ( 1.537181070339166844, 1.279018903020961329, 0.2500000000000000000 ) ) ;
#3383=EDGE_LOOP ( 'NONE', ( #5345, #4476, #6514, #5444 ) ) ;
#3386=CARTESIAN_POINT ( 'NONE',  ( 1.384649234319611288, 1.035652040038434807, -0.08212881570848259982 ) ) ;
#3387=CARTESIAN_POINT ( 'NONE',  ( 1.400692579910243429, 1.149720402410526976, 0.2179999999999999716 ) ) ;
#3393=ORIENTED_EDGE ( 'NONE', *, *, #6152, .T. ) ;
#3394=EDGE_CURVE ( 'NONE', #3711, #3298, #3042, .T. ) ;
#3397=DIRECTION ( 'NONE',  ( 0.9726399823210830631, 0.2323175946639496336, 0.000000000000000000 ) ) ;
#3399=CARTESIAN_POINT ( 'NONE',  ( 1.655550958614606438, 1.357113354811811057, 0.2318296825077736378 ) ) ;
#3403=EDGE_CURVE ( 'NONE', #4974, #1559, #4499, .T. ) ;
#3405=CARTESIAN_POINT ( 'NONE',  ( 1.290439921825005554, 1.657739327948754671, 0.2499999999999999722 ) ) ;
#3406=DIRECTION ( 'NONE',  ( 0.7879377495398141029, 0.6157549048526801405, 0.000000000000000000 ) ) ;
#3408=CYLINDRICAL_SURFACE ( 'NONE', #3752, 0.3750000000001075251 ) ;
#3413=CARTESIAN_POINT ( 'NONE',  ( 1.492515782973882432, 1.856045982048359688, -0.05383208248477879682 ) ) ;
#3416=CARTESIAN_POINT ( 'NONE',  ( 0.3566525292043902229, -0.3408511508279103985, 0.2216499829201352689 ) ) ;
#3417=CARTESIAN_POINT ( 'NONE',  ( 1.463490907143538688, 1.192314464452256972, 0.2277028927441933914 ) ) ;
#3421=CARTESIAN_POINT ( 'NONE',  ( 1.400692579910243651, 1.149720402410526754, 0.2500000000000000000 ) ) ;
#3423=DIRECTION ( 'NONE',  ( -1.000000000000000000, -1.762482576557733776E-15, 0.000000000000000000 ) ) ;
#3427=DIRECTION ( 'NONE',  ( -1.000000000000000000, 0.000000000000000000, 0.000000000000000000 ) ) ;
#3428=VERTEX_POINT ( 'NONE', #6209 ) ;
#3441=DIRECTION ( 'NONE',  ( 0.000000000000000000, 0.000000000000000000, -1.000000000000000000 ) ) ;
#3442=ORIENTED_EDGE ( 'NONE', *, *, #4050, .F. ) ;
#3444=CARTESIAN_POINT ( 'NONE',  ( 1.411244833761398310, 1.056435878372752324, -0.1949596646313069837 ) ) ;
#3446=CARTESIAN_POINT ( 'NONE',  ( -0.5068880400889234084, 2.974486634375206329, 0.000000000000000000 ) ) ;
#3450=CARTESIAN_POINT ( 'NONE',  ( 0.3265987596359649636, -0.3651148059186102857, 0.2456569822661065772 ) ) ;
#3451=CARTESIAN_POINT ( 'NONE',  ( 1.571814533976791495, 1.273076930690883124, 0.2372021369713644967 ) ) ;
#3452=ORIENTED_EDGE ( 'NONE', *, *, #3990, .F. ) ;
#3454=ORIENTED_EDGE ( 'NONE', *, *, #7151, .T. ) ;
#3457=CARTESIAN_POINT ( 'NONE',  ( -4.882388066182494768, 5.670153330992220297, 0.3125000000000000000 ) ) ;
#3458=CARTESIAN_POINT ( 'NONE',  ( 1.652539028737726179, 1.219618926967090289, -0.1039999999999998703 ) ) ;
#3461=ORIENTED_EDGE ( 'NONE', *, *, #4180, .T. ) ;
#3462=VERTEX_POINT ( 'NONE', #8073 ) ;
#3464=VECTOR ( 'NONE', #5258, 39.37007874015748854 ) ;
#3466=FACE_OUTER_BOUND ( 'NONE', #7816, .T. ) ;
#3471=EDGE_LOOP ( 'NONE', ( #6464, #5044, #1809, #59 ) ) ;
#3473=CARTESIAN_POINT ( 'NONE',  ( 2.036190745269639724, 1.255453516974595507, -0.08212881570848257207 ) ) ;
#3475=CIRCLE ( 'NONE', #6485, 0.3243589946935200308 ) ;
#3477=ADVANCED_FACE ( 'NONE', ( #5468 ), #7955, .T. ) ;
#3480=EDGE_CURVE ( 'NONE', #5415, #1006, #1618, .T. ) ;
#3481=DIRECTION ( 'NONE',  ( -1.000000000000000000, 0.000000000000000000, -0.000000000000000000 ) ) ;
#3485=AXIS2_PLACEMENT_3D ( 'NONE', #7328, #4956, #441 ) ;
#3495=CARTESIAN_POINT ( 'NONE',  ( 0.3495743270459968910, -0.3469141170041438738, 0.2327060356060121626 ) ) ;
#3497=CARTESIAN_POINT ( 'NONE',  ( -0.6570132742846659379, -0.6068321365170169512, 0.2500000000000000000 ) ) ;
#3501=VERTEX_POINT ( 'NONE', #784 ) ;
#3503=EDGE_LOOP ( 'NONE', ( #5892, #4854, #5145, #2140 ) ) ;
#3505=LINE ( 'NONE', #5426, #7560 ) ;
#3507=CARTESIAN_POINT ( 'NONE',  ( 1.859753234433174418, 1.471617347716406288, -0.009971652696953780398 ) ) ;
#3509=AXIS2_PLACEMENT_3D ( 'NONE', #3697, #7543, #3033 ) ;
#3511=CIRCLE ( 'NONE', #1023, 0.03200000000000009781 ) ;
#3529=EDGE_LOOP ( 'NONE', ( #5835, #2598, #5885, #3889 ) ) ;
#3534=EDGE_CURVE ( 'NONE', #3946, #7900, #5813, .T. ) ;
#3537=ORIENTED_EDGE ( 'NONE', *, *, #1127, .T. ) ;
#3542=CARTESIAN_POINT ( 'NONE',  ( 1.400692579912386826, 1.149720402407784059, 0.2179999999999999438 ) ) ;
#3548=CARTESIAN_POINT ( 'NONE',  ( 1.543023339786947723, 1.143323475675890322, 0.1681221971056049980 ) ) ;
#3553=DIRECTION ( 'NONE',  ( 0.9726399823210830631, 0.2323175946639496336, 0.000000000000000000 ) ) ;
#3554=CARTESIAN_POINT ( 'NONE',  ( 1.321405161348359947, 1.071700536256935843, -0.1133567676827914872 ) ) ;
#3555=AXIS2_PLACEMENT_3D ( 'NONE', #5720, #6981, #135 ) ;
#3559=ORIENTED_EDGE ( 'NONE', *, *, #7200, .T. ) ;
#3560=DIRECTION ( 'NONE',  ( -0.7879377495398142139, -0.6157549048526801405, 0.000000000000000000 ) ) ;
#3561=CIRCLE ( 'NONE', #292, 0.5000000000000279776 ) ;
#3564=CARTESIAN_POINT ( 'NONE',  ( 1.535032449692323997, 1.849374163788637837, -0.03177454249412108023 ) ) ;
#3570=CARTESIAN_POINT ( 'NONE',  ( 1.569959517566582363, 0.8504923821133684170, -0.08212881570848257207 ) ) ;
#3572=B_SPLINE_CURVE_WITH_KNOTS ( 'NONE', 3,
 ( #5625, #3242, #3902, #2654, #3781, #1890, #5160, #5046 ),
 .UNSPECIFIED., .F., .F.,
 ( 4, 2, 2, 4 ),
 ( 2.742838647325547832E-18, 0.0003234044359150124292, 0.0006468088718300220395, 0.001293617743660035839 ),
 .UNSPECIFIED. ) ;
#3574=VERTEX_POINT ( 'NONE', #7587 ) ;
#3579=CARTESIAN_POINT ( 'NONE',  ( 0.1009400014640523119, -0.4585254034878745721, 0.2212619352215731139 ) ) ;
#3582=AXIS2_PLACEMENT_3D ( 'NONE', #315, #6471, #2821 ) ;
#3587=FACE_OUTER_BOUND ( 'NONE', #1522, .T. ) ;
#3588=DIRECTION ( 'NONE',  ( 0.000000000000000000, 0.000000000000000000, -1.000000000000000000 ) ) ;
#3589=EDGE_CURVE ( 'NONE', #7415, #6720, #6347, .T. ) ;
#3595=VERTEX_POINT ( 'NONE', #5750 ) ;
#3599=CARTESIAN_POINT ( 'NONE',  ( 1.780616048947831098, 1.055727875058976251, -0.08212881570848259982 ) ) ;
#3603=VECTOR ( 'NONE', #5603, 39.37007874015748143 ) ;
#3604=LINE ( 'NONE', #4750, #6614 ) ;
#3609=CARTESIAN_POINT ( 'NONE',  ( 1.630463830202529829, 1.227750391954798070, 0.1987711295701233005 ) ) ;
#3611=CIRCLE ( 'NONE', #327, 0.3750000000000000555 ) ;
#3618=LINE ( 'NONE', #2458, #3872 ) ;
#3619=CARTESIAN_POINT ( 'NONE',  ( 1.570113095412482451, 1.303985922897850758, 0.2500000000000000555 ) ) ;
#3620=CIRCLE ( 'NONE', #5189, 0.2500000000000000555 ) ;
#3621=( BOUNDED_SURFACE ( )  B_SPLINE_SURFACE ( 3, 2, ( 
 ( #1170, #4908, #2983 ),
 ( #1623, #4172, #3548 ),
 ( #435, #5440, #7927 ),
 ( #2324, #4831, #2355 ),
 ( #7324, #1706, #3680 ),
 ( #516, #6709, #8005 ),
 ( #6753, #480, #4867 ),
 ( #3020, #6179, #1748 ),
 ( #4256, #552, #1139 ),
 ( #6142, #5518, #7408 ),
 ( #4296, #5368, #7624 ),
 ( #8088, #6493, #2012 ),
 ( #4950, #7673, #6407 ),
 ( #1210, #4982, #6364 ),
 ( #7449, #4519, #3719 ),
 ( #7020, #5175, #4373 ),
 ( #6226, #3251, #2062 ),
 ( #751, #2099, #4598 ) ),
 .UNSPECIFIED., .F., .F., .F. ) 
 B_SPLINE_SURFACE_WITH_KNOTS ( ( 4, 2, 2, 2, 2, 2, 2, 2, 4 ),
 ( 3, 3 ),
 ( 0.005269457407105175052, 0.006547192405793211822, 0.007824927404481247725, 0.009102662403169283628, 0.01038039740185731953, 0.01165813240054535543, 0.01293586739923339307, 0.01421360239792142897, 0.01549133739660946488 ),
 ( 0.1429062507207413957, 0.9470558914401250306 ),
 .UNSPECIFIED. ) 
 GEOMETRIC_REPRESENTATION_ITEM ( )  RATIONAL_B_SPLINE_SURFACE ( (
 ( 0.9282505022062121913, 0.7600379373203958178, 0.9706280646979809079),
 ( 0.9343171304435629043, 0.7803274260291386266, 0.9731115470576900961),
 ( 0.9397170595443995467, 0.7983871778769424665, 0.9753221042471091895),
 ( 0.9491101166107969167, 0.8298017162058096696, 0.9791673195158672183),
 ( 0.9531118816443266972, 0.8431853888632105942, 0.9808055133328683617),
 ( 0.9595828167972388911, 0.8648270587634172557, 0.9834545059321079252),
 ( 0.9620129929284466641, 0.8729546428587842133, 0.9844493418305206855),
 ( 0.9652734486511969081, 0.8838590492248784569, 0.9857840674730465880),
 ( 0.9661037643372263339, 0.8866359922115385483, 0.9861239719930808834),
 ( 0.9661130461342239961, 0.8866670346469766040, 0.9861277716620581169),
 ( 0.9652745230984527414, 0.8838626426518387813, 0.9857845073171743744),
 ( 0.9620007201733109525, 0.8729135973361294987, 0.9844443177595388894),
 ( 0.9595699749684953872, 0.8647841100068597298, 0.9834492489007055083),
 ( 0.9531660649921475104, 0.8433666019490960730, 0.9808276942516981345),
 ( 0.9491742944624668166, 0.8300163553341466383, 0.9791935918629224300),
 ( 0.9397117968768438079, 0.7983695771884257164, 0.9753199498803788448),
 ( 0.9342913856339358780, 0.7802413239962128211, 0.9731010079611670527),
 ( 0.9282505022067131240, 0.7600379373220710333, 0.9706280646981859661) ) ) 
 REPRESENTATION_ITEM ( '' )  SURFACE ( )  );
#3624=AXIS2_PLACEMENT_3D ( 'NONE', #5864, #1589, #2124 ) ;
#3626=CARTESIAN_POINT ( 'NONE',  ( 15385.36825653051164, -19685.23544977528218, -0.3750000000000000555 ) ) ;
#3628=ORIENTED_EDGE ( 'NONE', *, *, #3480, .F. ) ;
#3631=CARTESIAN_POINT ( 'NONE',  ( -1.040997396242601791, -0.7528336330030669377, 0.2179999999999999993 ) ) ;
#3634=ORIENTED_EDGE ( 'NONE', *, *, #482, .F. ) ;
#3637=CIRCLE ( 'NONE', #3509, 6.930657474112426719 ) ;
#3638=DIRECTION ( 'NONE',  ( 0.7879377495398141029, 0.6157549048526801405, 0.000000000000000000 ) ) ;
#3640=DIRECTION ( 'NONE',  ( 0.7879377495398141029, 0.6157549048526802515, 0.000000000000000000 ) ) ;
#3641=CIRCLE ( 'NONE', #5213, 0.1523203157102364369 ) ;
#3642=CARTESIAN_POINT ( 'NONE',  ( 1.528753255969025782, 1.853077197008292210, -0.02325729969694005292 ) ) ;
#3646=ADVANCED_FACE ( 'NONE', ( #6291 ), #3064, .T. ) ;
#3651=ADVANCED_FACE ( 'NONE', ( #4562 ), #3744, .T. ) ;
#3652=DIRECTION ( 'NONE',  ( 0.6157549048526803626, -0.7879377495398141029, 0.000000000000000000 ) ) ;
#3655=DIRECTION ( 'NONE',  ( -0.7879377495371227003, -0.6157549048561240523, -4.372694539034060785E-12 ) ) ;
#3656=CARTESIAN_POINT ( 'NONE',  ( 1.681711120206815346, 1.342581682021484424, 0.2165151474863769854 ) ) ;
#3660=DIRECTION ( 'NONE',  ( 0.4606913525677331367, 0.8875604078987031631, 0.000000000000000000 ) ) ;
#3661=ORIENTED_EDGE ( 'NONE', *, *, #5849, .F. ) ;
#3668=LINE ( 'NONE', #2465, #333 ) ;
#3670=( BOUNDED_SURFACE ( )  B_SPLINE_SURFACE ( 3, 2, ( 
 ( #3062, #2987, #2357 ),
 ( #7368, #8011, #4264 ),
 ( #5615, #6148, #520 ),
 ( #1799, #4914, #3023 ),
 ( #3722, #4301, #6231 ),
 ( #6796, #3554, #3684 ),
 ( #3113, #5956, #2482 ),
 ( #1871, #6875, #3307 ),
 ( #5198, #6309, #5027 ),
 ( #2522, #7605, #2077 ),
 ( #4542, #5735, #7697 ),
 ( #7531, #28, #110 ) ),
 .UNSPECIFIED., .F., .F., .F. ) 
 B_SPLINE_SURFACE_WITH_KNOTS ( ( 4, 2, 2, 2, 2, 4 ),
 ( 3, 3 ),
 ( 0.000000000000000000, 0.001554125582113249264, 0.002331188373169874005, 0.003108251164226498529, 0.004662376746339748010, 0.006216502328452997057 ),
 ( 0.000000000000000000, 1.000000000000000000 ),
 .UNSPECIFIED. ) 
 GEOMETRIC_REPRESENTATION_ITEM ( )  RATIONAL_B_SPLINE_SURFACE ( (
 ( 1.000000000000000000, 0.7071067811871933895, 1.000000000000000000),
 ( 1.000000000000000000, 0.7276057061276963722, 1.000000000000000000),
 ( 1.000000000000000000, 0.7554750547903839042, 1.000000000000000000),
 ( 1.000000000000000000, 0.8015396134353254265, 1.000000000000000000),
 ( 1.000000000000000000, 0.8174651680526996422, 1.000000000000000000),
 ( 1.000000000000000000, 0.8485784994800038561, 1.000000000000000000),
 ( 1.000000000000000000, 0.8638859094028720209, 1.000000000000000000),
 ( 1.000000000000000000, 0.9076931387944575658, 1.000000000000000000),
 ( 1.000000000000000000, 0.9340604879544870398, 1.000000000000000000),
 ( 1.000000000000000000, 0.9743637288758403292, 1.000000000000000000),
 ( 1.000000000000000000, 0.9885326174603896732, 1.000000000000000000),
 ( 1.000000000000000000, 0.9952915331365300711, 1.000000000000000000) ) ) 
 REPRESENTATION_ITEM ( '' )  SURFACE ( )  );
#3673=DIRECTION ( 'NONE',  ( -0.7879377495398138809, -0.6157549048526805846, 0.000000000000000000 ) ) ;
#3680=CARTESIAN_POINT ( 'NONE',  ( 1.576888795949508149, 1.175023536331549767, 0.1861679426474743271 ) ) ;
#3684=CARTESIAN_POINT ( 'NONE',  ( 1.334519317039704056, 1.071954003771020236, -0.09828849750274241959 ) ) ;
#3688=EDGE_CURVE ( 'NONE', #577, #4011, #6338, .T. ) ;
#3690=MANIFOLD_SOLID_BREP ( 'Boss-Extrude7', #191 ) ;
#3694=DIRECTION ( 'NONE',  ( 0.000000000000000000, 0.000000000000000000, -1.000000000000000000 ) ) ;
#3697=CARTESIAN_POINT ( 'NONE',  ( -4.882388066182508091, 5.670153330992292240, 0.03199999999999999373 ) ) ;
#3704=CARTESIAN_POINT ( 'NONE',  ( 1.854779829072218833, 1.467068431075036372, 0.01092961263066827109 ) ) ;
#3709=VECTOR ( 'NONE', #5117, 39.37007874015748143 ) ;
#3711=VERTEX_POINT ( 'NONE', #683 ) ;
#3712=CARTESIAN_POINT ( 'NONE',  ( 0.1250000000000000000, 1.530808498934191509E-17, 0.2500000000000000000 ) ) ;
#3714=AXIS2_PLACEMENT_3D ( 'NONE', #1062, #3560, #4268 ) ;
#3718=LINE ( 'NONE', #8002, #4260 ) ;
#3719=CARTESIAN_POINT ( 'NONE',  ( 1.724226450181035597, 1.288377220358824182, 0.1823870340488806252 ) ) ;
#3722=CARTESIAN_POINT ( 'NONE',  ( 1.300898271301138331, 1.089340557784379770, -0.1081788068622108884 ) ) ;
#3724=AXIS2_PLACEMENT_3D ( 'NONE', #7694, #4614, #5732 ) ;
#3725=CARTESIAN_POINT ( 'NONE',  ( 1.838053356874555622, 1.483773278494235015, 0.04018154866381434126 ) ) ;
#3727=DIRECTION ( 'NONE',  ( 1.000000000000000000, 0.000000000000000000, -0.000000000000000000 ) ) ;
#3728=CIRCLE ( 'NONE', #7390, 0.3045082206899650812 ) ;
#3735=CARTESIAN_POINT ( 'NONE',  ( 1.994799250004547719, 1.182494687089567620, -0.1039999999999998703 ) ) ;
#3744=CYLINDRICAL_SURFACE ( 'NONE', #314, 0.03199999999999994515 ) ;
#3747=CARTESIAN_POINT ( 'NONE',  ( -1.045359630492886938, -0.7381809969516824887, 0.2465270810310471739 ) ) ;
#3752=AXIS2_PLACEMENT_3D ( 'NONE', #3626, #5054, #6777 ) ;
#3754=CARTESIAN_POINT ( 'NONE',  ( 1.278468178840724834, 1.054204894366048473, -0.03540237177934978802 ) ) ;
#3756=CARTESIAN_POINT ( 'NONE',  ( -6.420602001755994159, -1.404684638105634820, 0.3125000000000000000 ) ) ;
#3757=DIRECTION ( 'NONE',  ( 0.6157549048526802515, -0.7879377495398142139, 0.000000000000000000 ) ) ;
#3759=CARTESIAN_POINT ( 'NONE',  ( -0.6570132742846659379, -0.6068321365170168402, 0.2179999999999999993 ) ) ;
#3762=ORIENTED_EDGE ( 'NONE', *, *, #6152, .F. ) ;
#3766=TOROIDAL_SURFACE ( 'NONE', #5205, 0.2704878104020024265, 0.03200000000000000067 ) ;
#3767=AXIS2_PLACEMENT_3D ( 'NONE', #3458, #2150, #5965 ) ;
#3768=ORIENTED_EDGE ( 'NONE', *, *, #1141, .T. ) ;
#3771=DIRECTION ( 'NONE',  ( -0.4606913525677331367, -0.8875604078987031631, -0.000000000000000000 ) ) ;
#3772=CIRCLE ( 'NONE', #1647, 0.03200000000000007006 ) ;
#3774=CIRCLE ( 'NONE', #3485, 0.1250000000000000000 ) ;
#3781=CARTESIAN_POINT ( 'NONE',  ( -1.200653967786500020, -0.2165511910659388140, 0.2437698526464839588 ) ) ;
#3782=VERTEX_POINT ( 'NONE', #3958 ) ;
#3783=CARTESIAN_POINT ( 'NONE',  ( 1.532760465343473877, 1.242737084437108841, 0.2356017578317803340 ) ) ;
#3790=ADVANCED_FACE ( 'NONE', ( #7643 ), #979, .T. ) ;
#3792=ORIENTED_EDGE ( 'NONE', *, *, #3403, .F. ) ;
#3797=EDGE_CURVE ( 'NONE', #5277, #5561, #2806, .T. ) ;
#3799=DIRECTION ( 'NONE',  ( -0.6568496200222102566, 0.7540216022612866720, 0.000000000000000000 ) ) ;
#3800=CARTESIAN_POINT ( 'NONE',  ( 1.652539028737726179, 1.219618926967090289, -0.1039999999999998703 ) ) ;
#3803=DIRECTION ( 'NONE',  ( -1.000000000000000000, 0.000000000000000000, 0.000000000000000000 ) ) ;
#3808=CARTESIAN_POINT ( 'NONE',  ( 1.844772722119052411, 1.489667545232676860, 0.02056656897901768324 ) ) ;
#3812=VERTEX_POINT ( 'NONE', #5237 ) ;
#3814=CARTESIAN_POINT ( 'NONE',  ( 1.536996473475150671, 1.850194254988873244, -0.04789697820840163600 ) ) ;
#3820=CARTESIAN_POINT ( 'NONE',  ( 1.782489676200804229, 1.410020151375938946, 0.1439750967038709029 ) ) ;
#3823=CARTESIAN_POINT ( 'NONE',  ( 1.520244955686326449, 1.863329565020348300, -0.0002333994861012334227 ) ) ;
#3824=EDGE_CURVE ( 'NONE', #3501, #2354, #6990, .T. ) ;
#3825=EDGE_CURVE ( 'NONE', #695, #4364, #7125, .T. ) ;
#3828=ADVANCED_FACE ( 'NONE', ( #5144, #107 ), #2563, .T. ) ;
#3829=DIRECTION ( 'NONE',  ( 0.2853335501257686646, -0.9584282785752022971, 0.000000000000000000 ) ) ;
#3831=CARTESIAN_POINT ( 'NONE',  ( 1.536996473475150671, 1.850194254988873244, -0.04789697820840163600 ) ) ;
#3832=DIRECTION ( 'NONE',  ( 0.2853335501257686646, -0.9584282785752022971, 0.000000000000000000 ) ) ;
#3841=EDGE_LOOP ( 'NONE', ( #1135, #6772, #7398, #1570 ) ) ;
#3842=CARTESIAN_POINT ( 'NONE',  ( 1.725050460137628194, 1.380013254716581761, 0.2019012614946010253 ) ) ;
#3851=VERTEX_POINT ( 'NONE', #7845 ) ;
#3861=ADVANCED_BREP_SHAPE_REPRESENTATION ( '', ( #3690, #3555 ), #2249 ) ;
#3865=AXIS2_PLACEMENT_3D ( 'NONE', #5026, #7263, #6308 ) ;
#3866=CARTESIAN_POINT ( 'NONE',  ( 1.640223930641419914, 1.235377681954054285, -0.08212881570848259982 ) ) ;
#3871=LINE ( 'NONE', #3296, #2949 ) ;
#3872=VECTOR ( 'NONE', #3660, 39.37007874015748143 ) ;
#3873=EDGE_CURVE ( 'NONE', #5314, #684, #7876, .T. ) ;
#3876=ORIENTED_EDGE ( 'NONE', *, *, #4953, .T. ) ;
#3884=ADVANCED_FACE ( 'NONE', ( #2160 ), #4736, .T. ) ;
#3885=EDGE_CURVE ( 'NONE', #7983, #2070, #5425, .T. ) ;
#3889=ORIENTED_EDGE ( 'NONE', *, *, #942, .F. ) ;
#3893=CARTESIAN_POINT ( 'NONE',  ( 1.823416444783682477, 1.453886705131341772, 0.09198493102659689724 ) ) ;
#3901=CIRCLE ( 'NONE', #6907, 0.03200000000000009781 ) ;
#3902=CARTESIAN_POINT ( 'NONE',  ( -1.197335310760672789, -0.2276984772474723306, 0.2492042935900711242 ) ) ;
#3903=VERTEX_POINT ( 'NONE', #4084 ) ;
#3915=ORIENTED_EDGE ( 'NONE', *, *, #4117, .T. ) ;
#3920=CARTESIAN_POINT ( 'NONE',  ( 1.676936960580814651, 1.351834804519730815, 0.2274697013873200890 ) ) ;
#3921=CARTESIAN_POINT ( 'NONE',  ( 0.9690125299525020885, 0.8529848947786566882, 0.2500000000000000000 ) ) ;
#3924=( BOUNDED_CURVE ( )  B_SPLINE_CURVE ( 3, ( #7770, #5324, #2163, #4740 ),
 .UNSPECIFIED., .F., .T. ) 
 B_SPLINE_CURVE_WITH_KNOTS ( ( 4, 4 ),
 ( 1.570796326794897668, 2.774242905800009318 ),
 .UNSPECIFIED. ) 
 CURVE ( )  GEOMETRIC_REPRESENTATION_ITEM ( )  RATIONAL_B_SPLINE_CURVE ( ( 1.000000000000000000, 0.8829075649559229300, 0.8829075649559229300, 1.000000000000000000 ) ) 
 REPRESENTATION_ITEM ( '' )  );
#3925=EDGE_CURVE ( 'NONE', #3222, #112, #4166, .T. ) ;
#3927=CARTESIAN_POINT ( 'NONE',  ( 1.508907770781040547, 1.868855936767433779, 0.03336486358077169617 ) ) ;
#3931=DIRECTION ( 'NONE',  ( 1.000000000000000000, 0.000000000000000000, 0.000000000000000000 ) ) ;
#3932=DIRECTION ( 'NONE',  ( 0.6157549048526804736, -0.7879377495398138809, 0.000000000000000000 ) ) ;
#3933=VERTEX_POINT ( 'NONE', #3542 ) ;
#3934=LINE ( 'NONE', #2610, #3709 ) ;
#3941=CARTESIAN_POINT ( 'NONE',  ( 1.877293513487986676, 1.420642010912031683, -0.07224819784990933746 ) ) ;
#3942=CARTESIAN_POINT ( 'NONE',  ( 1.434855324240962071, 1.174358127631301540, 0.2233288069132987330 ) ) ;
#3944=ORIENTED_EDGE ( 'NONE', *, *, #7041, .F. ) ;
#3945=LINE ( 'NONE', #5061, #2117 ) ;
#3946=VERTEX_POINT ( 'NONE', #5931 ) ;
#3958=CARTESIAN_POINT ( 'NONE',  ( -1.050138139902704104, -0.7221301030214424266, 0.000000000000000000 ) ) ;
#3959=ORIENTED_EDGE ( 'NONE', *, *, #1040, .T. ) ;
#3960=VECTOR ( 'NONE', #2460, 39.37007874015748143 ) ;
#3961=CARTESIAN_POINT ( 'NONE',  ( 1.571814533976791495, 1.273076930690883124, 0.2372021369713644967 ) ) ;
#3965=ORIENTED_EDGE ( 'NONE', *, *, #3992, .T. ) ;
#3968=CARTESIAN_POINT ( 'NONE',  ( 1.359242672892850390, 1.751896166577295633, 0.2197878876622516298 ) ) ;
#3972=VECTOR ( 'NONE', #4876, 39.37007874015748854 ) ;
#3974=CARTESIAN_POINT ( 'NONE',  ( -9.251037553912103917, -0.6017136928027502218, 0.3125000000000000000 ) ) ;
#3975=ORIENTED_EDGE ( 'NONE', *, *, #5028, .T. ) ;
#3978=AXIS2_PLACEMENT_3D ( 'NONE', #3457, #1532, #2263 ) ;
#3980=CARTESIAN_POINT ( 'NONE',  ( 1.260018307975525387, 1.633742302984368733, 0.2500000000000000000 ) ) ;
#3990=EDGE_CURVE ( 'NONE', #4011, #2564, #3728, .T. ) ;
#3992=EDGE_CURVE ( 'NONE', #6, #3812, #188, .T. ) ;
#3993=AXIS2_PLACEMENT_3D ( 'NONE', #1250, #2980, #4906 ) ;
#3999=CARTESIAN_POINT ( 'NONE',  ( 0.8135394388129589816, 1.284829519251779573, 0.000000000000000000 ) ) ;
#4003=CARTESIAN_POINT ( 'NONE',  ( 1.859621461000523945, 1.475107775274728361, -0.006828021556016123858 ) ) ;
#4004=ADVANCED_FACE ( 'NONE', ( #3466 ), #2547, .T. ) ;
#4005=VERTEX_POINT ( 'NONE', #3754 ) ;
#4008=AXIS2_PLACEMENT_3D ( 'NONE', #1588, #4094, #2282 ) ;
#4011=VERTEX_POINT ( 'NONE', #4250 ) ;
#4016=CARTESIAN_POINT ( 'NONE',  ( 1.579309947762197686, 1.291120561748658302, 0.2500517076223078283 ) ) ;
#4022=AXIS2_PLACEMENT_3D ( 'NONE', #4026, #5289, #3406 ) ;
#4024=PRODUCT ( 'Cleco, Handle, Pivoting', 'Cleco, Handle, Pivoting', '', ( #5558 ) ) ;
#4025=CARTESIAN_POINT ( 'NONE',  ( 1.861435943104858604, 1.485749338168939726, -0.007975310270593111497 ) ) ;
#4026=CARTESIAN_POINT ( 'NONE',  ( 1.723350842796532278, 1.129006085766179890, -0.1039999999999998703 ) ) ;
#4032=DIRECTION ( 'NONE',  ( -0.6157549048526823610, 0.7879377495398123266, 0.000000000000000000 ) ) ;
#4033=CIRCLE ( 'NONE', #100, 0.2500000000000000555 ) ;
#4039=EDGE_LOOP ( 'NONE', ( #571, #559, #2810, #2497 ) ) ;
#4044=CARTESIAN_POINT ( 'NONE',  ( 1.244866787915867912, 1.068558539350931369, -0.06210292240210582571 ) ) ;
#4046=CARTESIAN_POINT ( 'NONE',  ( 1.302790242782180918, 1.667167568704493341, -0.1039999999999998703 ) ) ;
#4050=EDGE_CURVE ( 'NONE', #4005, #577, #5552, .T. ) ;
#4053=ORIENTED_EDGE ( 'NONE', *, *, #823, .F. ) ;
#4058=DIRECTION ( 'NONE',  ( -0.6574491177601826664, -0.5137810939865956605, 0.5511711576436982840 ) ) ;
#4060=CARTESIAN_POINT ( 'NONE',  ( 1.753265575557962253, 1.417851156428476589, 0.1719230015339517637 ) ) ;
#4062=CARTESIAN_POINT ( 'NONE',  ( -0.1250000000000000000, 0.000000000000000000, 0.2500000000000000000 ) ) ;
#4066=DIRECTION ( 'NONE',  ( 0.000000000000000000, 0.000000000000000000, 1.000000000000000000 ) ) ;
#4069=CARTESIAN_POINT ( 'NONE',  ( 1.142655413120957197, 0.6307864494084283180, 0.000000000000000000 ) ) ;
#4070=CARTESIAN_POINT ( 'NONE',  ( 1.452776126473085183, 1.185506347940141092, 0.2257575757574807884 ) ) ;
#4075=ORIENTED_EDGE ( 'NONE', *, *, #4117, .F. ) ;
#4076=FACE_OUTER_BOUND ( 'NONE', #4853, .T. ) ;
#4077=CARTESIAN_POINT ( 'NONE',  ( 1.431357298810053358, 1.177565498724364446, 0.2499999999999698019 ) ) ;
#4079=CARTESIAN_POINT ( 'NONE',  ( 1.853159119997093596, 1.491110577246867797, -1.005434777941619967E-16 ) ) ;
#4080=ORIENTED_EDGE ( 'NONE', *, *, #8026, .F. ) ;
#4081=VERTEX_POINT ( 'NONE', #4288 ) ;
#4084=CARTESIAN_POINT ( 'NONE',  ( -1.499610808650658100, -1.013166758633947007, 0.3125000000000000000 ) ) ;
#4085=LINE ( 'NONE', #7320, #4375 ) ;
#4094=DIRECTION ( 'NONE',  ( -0.6157549048526802515, 0.7879377495398139919, -0.000000000000000000 ) ) ;
#4097=DIRECTION ( 'NONE',  ( -0.7879377495398137699, -0.6157549048526804736, 9.031266384036010773E-16 ) ) ;
#4098=ADVANCED_FACE ( 'NONE', ( #3587 ), #7136, .F. ) ;
#4101=VECTOR ( 'NONE', #407, 39.37007874015748143 ) ;
#4105=VERTEX_POINT ( 'NONE', #4860 ) ;
#4107=CARTESIAN_POINT ( 'NONE',  ( 0.3425853749674607762, -0.3527052086967336075, 0.2385123635927634544 ) ) ;
#4108=CARTESIAN_POINT ( 'NONE',  ( 1.447554089980937819, 1.218396913779240753, 0.2500000000000000000 ) ) ;
#4114=CARTESIAN_POINT ( 'NONE',  ( 1.863737827646003042, 1.449134593498074386, -0.03116755751364449697 ) ) ;
#4116=CARTESIAN_POINT ( 'NONE',  ( -1.041991915560238624, -0.7494930674187111341, 0.01525612839587352394 ) ) ;
#4117=EDGE_CURVE ( 'NONE', #4706, #3574, #1202, .T. ) ;
#4124=FACE_OUTER_BOUND ( 'NONE', #1849, .T. ) ;
#4130=DIRECTION ( 'NONE',  ( -0.6568496200222102566, 0.7540216022612866720, 0.000000000000000000 ) ) ;
#4132=ORIENTED_EDGE ( 'NONE', *, *, #4230, .T. ) ;
#4135=EDGE_CURVE ( 'NONE', #4276, #6720, #1902, .T. ) ;
#4138=AXIS2_PLACEMENT_3D ( 'NONE', #3076, #5582, #8064 ) ;
#4141=CIRCLE ( 'NONE', #1253, 0.4024878104020025438 ) ;
#4142=EDGE_CURVE ( 'NONE', #4722, #3812, #3050, .T. ) ;
#4143=EDGE_CURVE ( 'NONE', #4623, #3222, #4258, .T. ) ;
#4146=CARTESIAN_POINT ( 'NONE',  ( -1.196131363052349350, -0.2317425075729434292, -7.414317267960868635E-18 ) ) ;
#4155=CARTESIAN_POINT ( 'NONE',  ( 1.527344374864917365, 1.250631131126433537, 0.2500000000000000555 ) ) ;
#4156=AXIS2_PLACEMENT_3D ( 'NONE', #7948, #2340, #5271 ) ;
#4161=CARTESIAN_POINT ( 'NONE',  ( 1.437142212821967968, 1.212327995214759424, 0.2500000000000000000 ) ) ;
#4164=AXIS2_PLACEMENT_3D ( 'NONE', #7464, #6847, #1229 ) ;
#4165=TOROIDAL_SURFACE ( 'NONE', #3767, 0.4024878104020024328, 0.1000000000000000056 ) ;
#4166=LINE ( 'NONE', #6050, #4898 ) ;
#4167=CARTESIAN_POINT ( 'NONE',  ( -1.023858060246952029, -0.8104042351526981047, 0.3125000000000000000 ) ) ;
#4171=EDGE_LOOP ( 'NONE', ( #3304, #5203, #6129, #5101, #6969, #2019 ) ) ;
#4172=CARTESIAN_POINT ( 'NONE',  ( 1.495975307881522998, 1.195556502892835660, 0.1713108456322826045 ) ) ;
#4175=FACE_OUTER_BOUND ( 'NONE', #5807, .T. ) ;
#4179=CARTESIAN_POINT ( 'NONE',  ( 1.660036532843881085, 1.250860766742396324, 0.1987566293405836071 ) ) ;
#4180=EDGE_CURVE ( 'NONE', #3239, #1006, #1561, .T. ) ;
#4192=EDGE_CURVE ( 'NONE', #7906, #5277, #5167, .T. ) ;
#4199=CARTESIAN_POINT ( 'NONE',  ( 1.416910847748826363, 1.162394599040469156, 0.2206240621652085232 ) ) ;
#4202=CARTESIAN_POINT ( 'NONE',  ( 1.537647474970341932, 1.850702997413674389, 0.03199999999999999373 ) ) ;
#4203=EDGE_CURVE ( 'NONE', #7797, #7184, #5951, .T. ) ;
#4207=APPLICATION_CONTEXT ( 'configuration controlled 3d designs of mechanical parts and assemblies' ) ;
#4212=FACE_OUTER_BOUND ( 'NONE', #6656, .T. ) ;
#4214=B_SPLINE_CURVE_WITH_KNOTS ( 'NONE', 3,
 ( #7061, #3942, #6443, #826 ),
 .UNSPECIFIED., .F., .F.,
 ( 4, 4 ),
 ( 1.312212654013605714E-14, 0.001617146350552977566 ),
 .UNSPECIFIED. ) ;
#4215=ORIENTED_EDGE ( 'NONE', *, *, #7151, .F. ) ;
#4216=CARTESIAN_POINT ( 'NONE',  ( -4.882388066182508091, 5.670153330992292240, 0.2179999999999999993 ) ) ;
#4223=CARTESIAN_POINT ( 'NONE',  ( -1.200662090268964421, -0.2165239078499182623, 0.006252944700127002244 ) ) ;
#4224=CARTESIAN_POINT ( 'NONE',  ( 1.639694973349331120, 1.319210621310791920, 0.2298487237779671677 ) ) ;
#4230=EDGE_CURVE ( 'NONE', #4985, #810, #320, .T. ) ;
#4231=DIRECTION ( 'NONE',  ( -0.6930146854867019757, -0.5415747525367520243, 0.4758439167568747630 ) ) ;
#4237=DIRECTION ( 'NONE',  ( 0.6157549048526804736, -0.7879377495398138809, 0.000000000000000000 ) ) ;
#4239=FACE_OUTER_BOUND ( 'NONE', #7395, .T. ) ;
#4248=ORIENTED_EDGE ( 'NONE', *, *, #1040, .F. ) ;
#4250=CARTESIAN_POINT ( 'NONE',  ( 1.400290408515991292, 1.047875251497336402, -0.1039999999999998703 ) ) ;
#4252=CARTESIAN_POINT ( 'NONE',  ( 0.04629178820765882107, -0.4636611426331366248, 0.01068174274968844602 ) ) ;
#4255=CARTESIAN_POINT ( 'NONE',  ( 1.517690421940173007, 1.264920623133992006, 0.2499999999999999167 ) ) ;
#4256=CARTESIAN_POINT ( 'NONE',  ( 1.583224725446250369, 1.282100267436459884, 0.2376555858899458973 ) ) ;
#4258=CIRCLE ( 'NONE', #6346, 4.000000000000000888 ) ;
#4259=DIRECTION ( 'NONE',  ( 1.000000000000000000, 0.000000000000000000, 0.000000000000000000 ) ) ;
#4260=VECTOR ( 'NONE', #6751, 39.37007874015747433 ) ;
#4264=CARTESIAN_POINT ( 'NONE',  ( 1.288576881684712072, 1.062104608988174492, -0.04610097113422258197 ) ) ;
#4265=CARTESIAN_POINT ( 'NONE',  ( 1.800320205903116921, 1.030513867073702183, -0.08212881570848259982 ) ) ;
#4266=ORIENTED_EDGE ( 'NONE', *, *, #729, .F. ) ;
#4267=ORIENTED_EDGE ( 'NONE', *, *, #2080, .T. ) ;
#4268=DIRECTION ( 'NONE',  ( 0.6157549048526729241, -0.7879377495398196540, 0.000000000000000000 ) ) ;
#4271=AXIS2_PLACEMENT_3D ( 'NONE', #2549, #2710, #6441 ) ;
#4275=CYLINDRICAL_SURFACE ( 'NONE', #3091, 4.000000000000000888 ) ;
#4276=VERTEX_POINT ( 'NONE', #7137 ) ;
#4278=AXIS2_PLACEMENT_3D ( 'NONE', #199, #2825, #5909 ) ;
#4282=DIRECTION ( 'NONE',  ( 0.7879377495398141029, 0.6157549048526802515, 0.000000000000000000 ) ) ;
#4287=ADVANCED_FACE ( 'NONE', ( #2705 ), #7712, .T. ) ;
#4288=CARTESIAN_POINT ( 'NONE',  ( 1.640223930654117312, 1.235377681993896193, -0.4064878104020026583 ) ) ;
#4294=CARTESIAN_POINT ( 'NONE',  ( 1.559972549391304364, 1.821735304801280986, -0.05091778041741192723 ) ) ;
#4296=CARTESIAN_POINT ( 'NONE',  ( 1.621159559802907379, 1.311822379805967387, 0.2374608280823977957 ) ) ;
#4297=FACE_OUTER_BOUND ( 'NONE', #7637, .T. ) ;
#4298=ORIENTED_EDGE ( 'NONE', *, *, #5692, .F. ) ;
#4301=CARTESIAN_POINT ( 'NONE',  ( 1.308306517172985961, 1.069052077891893493, -0.1016069337487079394 ) ) ;
#4305=FACE_OUTER_BOUND ( 'NONE', #193, .T. ) ;
#4317=CARTESIAN_POINT ( 'NONE',  ( -4.521705384338368994, -3.437882612028420048, 0.000000000000000000 ) ) ;
#4320=ORIENTED_EDGE ( 'NONE', *, *, #942, .T. ) ;
#4328=CARTESIAN_POINT ( 'NONE',  ( 1.537180804724851413, 1.279018702714873612, 0.2500000000000000555 ) ) ;
#4337=ADVANCED_FACE ( 'NONE', ( #6070 ), #1358, .T. ) ;
#4339=DIRECTION ( 'NONE',  ( -0.6157549048526802515, 0.7879377495398141029, -0.000000000000000000 ) ) ;
#4342=EDGE_CURVE ( 'NONE', #822, #1921, #3005, .T. ) ;
#4347=CARTESIAN_POINT ( 'NONE',  ( 1.667733449989331929, 1.335098490384043712, 0.2216602983319173603 ) ) ;
#4352=DIRECTION ( 'NONE',  ( 0.6157549048509018963, -0.7879377495412036581, 0.000000000000000000 ) ) ;
#4364=VERTEX_POINT ( 'NONE', #6675 ) ;
#4365=CIRCLE ( 'NONE', #7755, 0.03200000000000000761 ) ;
#4367=CARTESIAN_POINT ( 'NONE',  ( 1.525041352626022473, 0.8560022331433567722, -0.08212881570848259982 ) ) ;
#4368=CIRCLE ( 'NONE', #1877, 3.939999999999463487 ) ;
#4369=CARTESIAN_POINT ( 'NONE',  ( 0.02203360116805245725, -0.4639491064115316976, 0.005840653693852291065 ) ) ;
#4371=CARTESIAN_POINT ( 'NONE',  ( 0.8923633780935225079, 0.7607014108325281798, 0.03200000000000000067 ) ) ;
#4372=CARTESIAN_POINT ( 'NONE',  ( 1.689090369710469330, 1.679451071328251333, 4.008942324862821895E-14 ) ) ;
#4373=CARTESIAN_POINT ( 'NONE',  ( 1.743841527944330894, 1.301069857420130038, 0.1733065278142748578 ) ) ;
#4374=ORIENTED_EDGE ( 'NONE', *, *, #2372, .T. ) ;
#4375=VECTOR ( 'NONE', #473, 39.37007874015748143 ) ;
#4376=AXIS2_PLACEMENT_3D ( 'NONE', #1733, #4237, #2463 ) ;
#4382=LINE ( 'NONE', #1874, #5527 ) ;
#4383=ORIENTED_EDGE ( 'NONE', *, *, #1668, .F. ) ;
#4386=ORIENTED_EDGE ( 'NONE', *, *, #7838, .T. ) ;
#4387=VECTOR ( 'NONE', #1519, 39.37007874015748143 ) ;
#4392=CARTESIAN_POINT ( 'NONE',  ( 1.738743531207847193, 1.407258481967477604, 0.1849942679939103052 ) ) ;
#4395=ORIENTED_EDGE ( 'NONE', *, *, #1186, .F. ) ;
#4396=CARTESIAN_POINT ( 'NONE',  ( 1.414905630928118274, 1.059296705655214499, -0.2064098076014010408 ) ) ;
#4401=CARTESIAN_POINT ( 'NONE',  ( 1.452776126472616669, 1.185506347939969674, 0.2257575757582501175 ) ) ;
#4403=EDGE_CURVE ( 'NONE', #4688, #5571, #3347, .T. ) ;
#4404=ADVANCED_FACE ( 'NONE', ( #2217 ), #5698, .T. ) ;
#4407=CARTESIAN_POINT ( 'NONE',  ( 1.302790242782180918, 1.667167568704493341, -0.1039999999999998703 ) ) ;
#4409=DIRECTION ( 'NONE',  ( -1.000000000000000000, 0.000000000000000000, 0.000000000000000000 ) ) ;
#4413=AXIS2_PLACEMENT_3D ( 'NONE', #7539, #2577, #3313 ) ;
#4414=AXIS2_PLACEMENT_3D ( 'NONE', #6933, #706, #4514 ) ;
#4415=ORIENTED_EDGE ( 'NONE', *, *, #7399, .F. ) ;
#4416=CARTESIAN_POINT ( 'NONE',  ( 1.603331916026614845, 1.035214104258893153, -0.1039999999999998564 ) ) ;
#4417=CARTESIAN_POINT ( 'NONE',  ( 1.640223930641419914, 1.235377681954054285, -0.08212881570848259982 ) ) ;
#4420=CARTESIAN_POINT ( 'NONE',  ( 1.566356832197602467, 1.820341369176796009, 2.344234228102034760E-14 ) ) ;
#4421=ORIENTED_EDGE ( 'NONE', *, *, #1440, .T. ) ;
#4429=CYLINDRICAL_SURFACE ( 'NONE', #2775, 0.03199999999999997985 ) ;
#4438=DIRECTION ( 'NONE',  ( -0.6157549048526803626, 0.7879377495398141029, -0.000000000000000000 ) ) ;
#4440=EDGE_CURVE ( 'NONE', #1006, #2215, #5829, .T. ) ;
#4448=ORIENTED_EDGE ( 'NONE', *, *, #6830, .F. ) ;
#4452=CARTESIAN_POINT ( 'NONE',  ( 1.949881085063987829, 1.188004538119556086, -0.1039999999999998703 ) ) ;
#4456=ORIENTED_EDGE ( 'NONE', *, *, #3081, .F. ) ;
#4459=CARTESIAN_POINT ( 'NONE',  ( 1.697905879539435725, 1.363584050841088358, 0.2176101576819327310 ) ) ;
#4461=CARTESIAN_POINT ( 'NONE',  ( 1.778571697411903907, 1.436640564646076035, 0.1446028122283900819 ) ) ;
#4476=ORIENTED_EDGE ( 'NONE', *, *, #1216, .F. ) ;
#4477=CARTESIAN_POINT ( 'NONE',  ( 0.9207653111462810180, 0.7459592875503607834, 0.03199999999999999373 ) ) ;
#4494=DIRECTION ( 'NONE',  ( 0.7879377495398137699, 0.6157549048526805846, 0.000000000000000000 ) ) ;
#4499=CIRCLE ( 'NONE', #973, 0.03200000000000002148 ) ;
#4504=CARTESIAN_POINT ( 'NONE',  ( 1.487026048750669238, 1.851755883273100922, 0.02040206030734219994 ) ) ;
#4505=CARTESIAN_POINT ( 'NONE',  ( 1.895798626963228317, 1.435103323869673764, -0.08212881570848257207 ) ) ;
#4509=CARTESIAN_POINT ( 'NONE',  ( 2.030680894239651479, 1.210535352034035839, -0.08212881570848259982 ) ) ;
#4514=DIRECTION ( 'NONE',  ( -1.000000000000000000, 0.000000000000000000, 0.000000000000000000 ) ) ;
#4516=CARTESIAN_POINT ( 'NONE',  ( 1.335403689192364851, 0.9717850835686417943, -0.1039999999999998703 ) ) ;
#4517=AXIS2_PLACEMENT_3D ( 'NONE', #7327, #2896, #6670 ) ;
#4519=CARTESIAN_POINT ( 'NONE',  ( 1.693285456672191325, 1.338775588042468767, 0.1841458301845965428 ) ) ;
#4526=FACE_OUTER_BOUND ( 'NONE', #1412, .T. ) ;
#4528=AXIS2_PLACEMENT_3D ( 'NONE', #2798, #6000, #371 ) ;
#4532=EDGE_CURVE ( 'NONE', #3239, #4688, #3611, .T. ) ;
#4533=EDGE_CURVE ( 'NONE', #4660, #822, #696, .T. ) ;
#4534=AXIS2_PLACEMENT_3D ( 'NONE', #1514, #5373, #2246 ) ;
#4541=CARTESIAN_POINT ( 'NONE',  ( 1.634230631622952457, 1.327686990689322277, 0.2415108169663792437 ) ) ;
#4542=CARTESIAN_POINT ( 'NONE',  ( 1.402435059179732990, 1.065697847451554825, -0.1946357965901184539 ) ) ;
#4548=AXIS2_PLACEMENT_3D ( 'NONE', #1910, #642, #1249 ) ;
#4549=CIRCLE ( 'NONE', #2057, 7.490657474112464520 ) ;
#4562=FACE_OUTER_BOUND ( 'NONE', #2312, .T. ) ;
#4574=ORIENTED_EDGE ( 'NONE', *, *, #5539, .F. ) ;
#4575=CARTESIAN_POINT ( 'NONE',  ( 1.697466594803655804, 1.379849898015399035, 0.2127906551866314833 ) ) ;
#4580=ORIENTED_EDGE ( 'NONE', *, *, #7300, .T. ) ;
#4581=CARTESIAN_POINT ( 'NONE',  ( 1.528725049572218664, 1.845702208139184064, 0.03396726950201266887 ) ) ;
#4582=DIRECTION ( 'NONE',  ( 0.000000000000000000, 0.000000000000000000, -1.000000000000000000 ) ) ;
#4584=ADVANCED_FACE ( 'NONE', ( #6194 ), #5078, .T. ) ;
#4590=CARTESIAN_POINT ( 'NONE',  ( -0.6495791112554195612, -0.6379566159512914947, 0.2179999999999999993 ) ) ;
#4592=ADVANCED_FACE ( 'NONE', ( #7129 ), #1979, .T. ) ;
#4594=CARTESIAN_POINT ( 'NONE',  ( 1.537935346170436812, 1.852967428140057216, 0.000000000000000000 ) ) ;
#4596=ORIENTED_EDGE ( 'NONE', *, *, #482, .T. ) ;
#4598=CARTESIAN_POINT ( 'NONE',  ( 1.761384412048883741, 1.314317347873839692, 0.1623010253713057793 ) ) ;
#4599=EDGE_LOOP ( 'NONE', ( #50, #2281 ) ) ;
#4600=( NAMED_UNIT ( * ) SI_UNIT ( $, .STERADIAN. ) SOLID_ANGLE_UNIT ( ) );
#4601=CYLINDRICAL_SURFACE ( 'NONE', #3978, 6.870657474112407570 ) ;
#4608=EDGE_LOOP ( 'NONE', ( #4674, #5554, #2730, #5501 ) ) ;
#4614=DIRECTION ( 'NONE',  ( 0.7013568910933712930, 0.4952151427499992820, -0.5126992039265700907 ) ) ;
#4623=VERTEX_POINT ( 'NONE', #1671 ) ;
#4624=CARTESIAN_POINT ( 'NONE',  ( 1.788409570110391256, 1.426923381411736358, 0.1429701060512907629 ) ) ;
#4625=DIRECTION ( 'NONE',  ( 0.7879377495385916363, 0.6157549048542446668, 0.000000000000000000 ) ) ;
#4629=FACE_OUTER_BOUND ( 'NONE', #7441, .T. ) ;
#4630=FACE_OUTER_BOUND ( 'NONE', #2402, .T. ) ;
#4632=ORIENTED_EDGE ( 'NONE', *, *, #1029, .F. ) ;
#4635=ADVANCED_FACE ( 'NONE', ( #4175 ), #7290, .F. ) ;
#4644=CARTESIAN_POINT ( 'NONE',  ( 0.3037060500451564393, -0.3811688768094762536, 0.2500000000000003331 ) ) ;
#4646=ADVANCED_FACE ( 'NONE', ( #7206 ), #5405, .T. ) ;
#4651=ORIENTED_EDGE ( 'NONE', *, *, #2084, .F. ) ;
#4657=CARTESIAN_POINT ( 'NONE',  ( 1.858819419417630847, 1.479091072822390718, -0.004310541304807894401 ) ) ;
#4658=CIRCLE ( 'NONE', #6621, 0.3099999999999745737 ) ;
#4659=AXIS2_PLACEMENT_3D ( 'NONE', #5371, #7851, #440 ) ;
#4660=VERTEX_POINT ( 'NONE', #1057 ) ;
#4666=LINE ( 'NONE', #7042, #2376 ) ;
#4670=CARTESIAN_POINT ( 'NONE',  ( 1.807005629368180655, 1.428622671733608129, 0.1122175490488539484 ) ) ;
#4674=ORIENTED_EDGE ( 'NONE', *, *, #7875, .F. ) ;
#4676=CARTESIAN_POINT ( 'NONE',  ( 1.399572429561498188, 1.060126801036724631, -0.1797357540389955821 ) ) ;
#4677=CIRCLE ( 'NONE', #1931, 0.03200000000000005618 ) ;
#4680=CARTESIAN_POINT ( 'NONE',  ( 1.536310283592701609, 1.851420836617818422, -0.007424632097850032350 ) ) ;
#4683=DIRECTION ( 'NONE',  ( -0.7879377495398141029, -0.6157549048526802515, 0.000000000000000000 ) ) ;
#4684=EDGE_CURVE ( 'NONE', #2070, #5954, #3604, .T. ) ;
#4686=CARTESIAN_POINT ( 'NONE',  ( 1.437142212823544263, 1.212327995211806453, 0.2500000000000000000 ) ) ;
#4687=ADVANCED_FACE ( 'NONE', ( #6594 ), #362, .F. ) ;
#4688=VERTEX_POINT ( 'NONE', #321 ) ;
#4692=FACE_OUTER_BOUND ( 'NONE', #1378, .T. ) ;
#4693=CARTESIAN_POINT ( 'NONE',  ( 1.850068364776406682, 1.494658567734585608, 0.000000000000000000 ) ) ;
#4696=ADVANCED_FACE ( 'NONE', ( #1709 ), #6488, .T. ) ;
#4697=ORIENTED_EDGE ( 'NONE', *, *, #5738, .T. ) ;
#4702=CARTESIAN_POINT ( 'NONE',  ( 15385.63906443092310, -19685.02381974099626, -0.2249973011472257700 ) ) ;
#4704=DIRECTION ( 'NONE',  ( 0.2853335501257686646, -0.9584282785752022971, 0.000000000000000000 ) ) ;
#4705=LINE ( 'NONE', #7204, #1348 ) ;
#4706=VERTEX_POINT ( 'NONE', #6109 ) ;
#4711=ORIENTED_EDGE ( 'NONE', *, *, #7480, .T. ) ;
#4717=DIRECTION ( 'NONE',  ( 1.000000000000000000, 0.000000000000000000, 0.000000000000000000 ) ) ;
#4718=FACE_OUTER_BOUND ( 'NONE', #2311, .T. ) ;
#4719=EDGE_LOOP ( 'NONE', ( #5982, #6789, #2579, #2635 ) ) ;
#4722=VERTEX_POINT ( 'NONE', #2399 ) ;
#4723=CARTESIAN_POINT ( 'NONE',  ( 1.872635725948145646, 1.428537503602546721, -0.05220482834521919524 ) ) ;
#4724=CARTESIAN_POINT ( 'NONE',  ( -1.045535649164317071, -0.7375897546243017633, 0.004036567931050074297 ) ) ;
#4726=DIRECTION ( 'NONE',  ( -0.6157549048526803626, 0.7879377495398141029, -0.000000000000000000 ) ) ;
#4730=ORIENTED_EDGE ( 'NONE', *, *, #7588, .F. ) ;
#4734=EDGE_CURVE ( 'NONE', #4105, #3222, #461, .T. ) ;
#4736=CYLINDRICAL_SURFACE ( 'NONE', #6216, 0.3099999999999745737 ) ;
#4740=CARTESIAN_POINT ( 'NONE',  ( 1.492904096916551460, 1.856349440303736831, -0.001813861035895662039 ) ) ;
#4743=DIRECTION ( 'NONE',  ( 1.000000000000000000, 0.000000000000000000, -0.000000000000000000 ) ) ;
#4750=CARTESIAN_POINT ( 'NONE',  ( 0.09537553527426730071, -0.4271221084841553273, 0.2500000000000000000 ) ) ;
#4752=CARTESIAN_POINT ( 'NONE',  ( -6.110602001756019419, -1.404684638105634820, -0.05999999999999999778 ) ) ;
#4753=CARTESIAN_POINT ( 'NONE',  ( 0.3517695222503834374, -0.3450570238940762757, 0.01951625562141530781 ) ) ;
#4758=CARTESIAN_POINT ( 'NONE',  ( -1.204376266962890796, -0.2040480809676099017, 0.03199999999999999373 ) ) ;
#4763=CARTESIAN_POINT ( 'NONE',  ( 1.492515782973968363, 1.856045982048426746, -0.05383208248535607116 ) ) ;
#4766=( BOUNDED_CURVE ( )  B_SPLINE_CURVE ( 3, ( #4594, #7094, #7746, #3980 ),
 .UNSPECIFIED., .F., .T. ) 
 B_SPLINE_CURVE_WITH_KNOTS ( ( 4, 4 ),
 ( 3.481429563043914932, 4.712388980384689674 ),
 .UNSPECIFIED. ) 
 CURVE ( )  GEOMETRIC_REPRESENTATION_ITEM ( )  RATIONAL_B_SPLINE_CURVE ( ( 1.000000000000000000, 0.8776643872851506156, 0.8776643872851506156, 1.000000000000000000 ) ) 
 REPRESENTATION_ITEM ( '' )  );
#4768=AXIS2_PLACEMENT_3D ( 'NONE', #3800, #6785, #1166 ) ;
#4770=CARTESIAN_POINT ( 'NONE',  ( 1.859928773101481303, 1.466967662321851718, -0.01415936195527345114 ) ) ;
#4787=DIRECTION ( 'NONE',  ( 0.000000000000000000, 0.000000000000000000, 1.000000000000000000 ) ) ;
#4800=DIRECTION ( 'NONE',  ( 0.000000000000000000, 0.000000000000000000, 1.000000000000000000 ) ) ;
#4802=CIRCLE ( 'NONE', #7162, 0.03200000000000005618 ) ;
#4805=DIRECTION ( 'NONE',  ( 0.7879377495398137699, 0.6157549048526804736, 0.000000000000000000 ) ) ;
#4806=DIRECTION ( 'NONE',  ( 0.000000000000000000, 0.000000000000000000, -1.000000000000000000 ) ) ;
#4808=ORIENTED_EDGE ( 'NONE', *, *, #4734, .T. ) ;
#4809=CARTESIAN_POINT ( 'NONE',  ( 2.055894902224925769, 1.230239508989321440, -0.08212881570848257207 ) ) ;
#4811=DIRECTION ( 'NONE',  ( -0.000000000000000000, -0.000000000000000000, -1.000000000000000000 ) ) ;
#4813=AXIS2_PLACEMENT_3D ( 'NONE', #1323, #3176, #7565 ) ;
#4814=EDGE_LOOP ( 'NONE', ( #7124, #5451, #5152, #2843 ) ) ;
#4817=EDGE_LOOP ( 'NONE', ( #7689, #6599, #4267, #2161, #2734, #1411, #1632, #4892, #7363, #6541, #7686, #7331 ) ) ;
#4821=DIRECTION ( 'NONE',  ( 0.7879377495398141029, 0.6157549048526801405, 0.000000000000000000 ) ) ;
#4822=AXIS2_PLACEMENT_3D ( 'NONE', #3075, #1307, #5581 ) ;
#4823=ORIENTED_EDGE ( 'NONE', *, *, #5849, .T. ) ;
#4824=B_SPLINE_CURVE_WITH_KNOTS ( 'NONE', 3,
 ( #3814, #5156, #1511, #1630, #984, #5372 ),
 .UNSPECIFIED., .F., .F.,
 ( 4, 2, 4 ),
 ( 7.607273545336762758E-15, 0.0006113010686663716007, 0.001222602137325135788 ),
 .UNSPECIFIED. ) ;
#4827=CARTESIAN_POINT ( 'NONE',  ( 1.640223930641419914, 1.235377681954054285, -0.08212881570848259982 ) ) ;
#4831=CARTESIAN_POINT ( 'NONE',  ( 1.526921265547024120, 1.208805900097675856, 0.1840890058364192117 ) ) ;
#4836=CARTESIAN_POINT ( 'NONE',  ( 1.142655413120957197, 0.6307864494084283180, 0.03199999999999999373 ) ) ;
#4837=VERTEX_POINT ( 'NONE', #6274 ) ;
#4841=EDGE_CURVE ( 'NONE', #6242, #5571, #2924, .T. ) ;
#4846=EDGE_CURVE ( 'NONE', #5314, #7717, #5419, .T. ) ;
#4853=EDGE_LOOP ( 'NONE', ( #244, #6532, #4415, #2302 ) ) ;
#4854=ORIENTED_EDGE ( 'NONE', *, *, #5739, .F. ) ;
#4856=CARTESIAN_POINT ( 'NONE',  ( 0.04627948923991306168, -0.4636619226355729873, 0.2393213367346657128 ) ) ;
#4859=ORIENTED_EDGE ( 'NONE', *, *, #4533, .F. ) ;
#4860=CARTESIAN_POINT ( 'NONE',  ( -0.6570132742846659379, -0.6068321365170168402, 0.000000000000000000 ) ) ;
#4862=CARTESIAN_POINT ( 'NONE',  ( 0.09906724953193619954, -0.4587982231398470834, 0.02730009524027248238 ) ) ;
#4866=ORIENTED_EDGE ( 'NONE', *, *, #5386, .F. ) ;
#4867=CARTESIAN_POINT ( 'NONE',  ( 1.603337854698916320, 1.200890287003202328, 0.1947064082056160772 ) ) ;
#4868=CARTESIAN_POINT ( 'NONE',  ( 1.586137004846402077, 0.9037470550431118133, -0.1039999999999998287 ) ) ;
#4874=ORIENTED_EDGE ( 'NONE', *, *, #4230, .F. ) ;
#4876=DIRECTION ( 'NONE',  ( 0.7879377495398141029, 0.6157549048526800295, 0.000000000000000000 ) ) ;
#4878=DIRECTION ( 'NONE',  ( -0.6157549048526801405, 0.7879377495398142139, 0.000000000000000000 ) ) ;
#4892=ORIENTED_EDGE ( 'NONE', *, *, #280, .T. ) ;
#4897=AXIS2_PLACEMENT_3D ( 'NONE', #1908, #3217, #3829 ) ;
#4898=VECTOR ( 'NONE', #3397, 39.37007874015748143 ) ;
#4906=DIRECTION ( 'NONE',  ( 1.000000000000000000, 0.000000000000000000, 0.000000000000000000 ) ) ;
#4908=CARTESIAN_POINT ( 'NONE',  ( 1.486276370885186937, 1.194002588456842373, 0.1672982580699348132 ) ) ;
#4911=ORIENTED_EDGE ( 'NONE', *, *, #6931, .F. ) ;
#4914=CARTESIAN_POINT ( 'NONE',  ( 1.301886230480333584, 1.067115050693573819, -0.09588550097992007415 ) ) ;
#4924=ORIENTED_EDGE ( 'NONE', *, *, #4143, .F. ) ;
#4932=CIRCLE ( 'NONE', #6765, 0.1523203157102364369 ) ;
#4933=CARTESIAN_POINT ( 'NONE',  ( 1.684866161243239846, 1.178252195112418299, -0.1039999999999998703 ) ) ;
#4935=ADVANCED_FACE ( 'NONE', ( #5146 ), #6703, .T. ) ;
#4938=EDGE_CURVE ( 'NONE', #4722, #1300, #2010, .T. ) ;
#4939=ORIENTED_EDGE ( 'NONE', *, *, #3338, .F. ) ;
#4942=CARTESIAN_POINT ( 'NONE',  ( -1.499610808650658100, -1.013166758633947007, -0.05999999999999999778 ) ) ;
#4944=VECTOR ( 'NONE', #6650, 39.37007874015748143 ) ;
#4945=CARTESIAN_POINT ( 'NONE',  ( -0.03921911030312474900, -0.4592703903598064352, 0.000000000000000000 ) ) ;
#4947=CARTESIAN_POINT ( 'NONE',  ( 0.8135394388118154518, 1.284829519253825492, -0.3750000000000000555 ) ) ;
#4948=DIRECTION ( 'NONE',  ( 0.000000000000000000, 0.000000000000000000, -1.000000000000000000 ) ) ;
#4950=CARTESIAN_POINT ( 'NONE',  ( 1.657918913468165778, 1.341234511226818471, 0.2362032458804501078 ) ) ;
#4953=EDGE_CURVE ( 'NONE', #4276, #4688, #1016, .T. ) ;
#4956=DIRECTION ( 'NONE',  ( 0.000000000000000000, 0.000000000000000000, 1.000000000000000000 ) ) ;
#4961=ORIENTED_EDGE ( 'NONE', *, *, #374, .F. ) ;
#4968=CARTESIAN_POINT ( 'NONE',  ( -1.750746777110393282, 1.631196835986985505, -0.05999999999999999778 ) ) ;
#4971=DIRECTION ( 'NONE',  ( 0.6157549048526801405, -0.7879377495398142139, -0.000000000000000000 ) ) ;
#4974=VERTEX_POINT ( 'NONE', #2889 ) ;
#4976=CARTESIAN_POINT ( 'NONE',  ( 1.313749575516037105, 1.070113901150813174, -0.07404765044330269275 ) ) ;
#4980=FACE_OUTER_BOUND ( 'NONE', #1495, .T. ) ;
#4982=CARTESIAN_POINT ( 'NONE',  ( 1.684660674153190429, 1.329988278726413009, 0.1880212863749382568 ) ) ;
#4984=ADVANCED_FACE ( 'NONE', ( #4124 ), #6051, .T. ) ;
#4985=VERTEX_POINT ( 'NONE', #357 ) ;
#4988=EDGE_CURVE ( 'NONE', #7063, #6859, #6555, .T. ) ;
#4992=B_SPLINE_CURVE_WITH_KNOTS ( 'NONE', 3,
 ( #7177, #812, #5819, #863, #1590, #2091, #6479, #6562, #4753, #3368, #7086, #7251 ),
 .UNSPECIFIED., .F., .F.,
 ( 4, 2, 2, 2, 2, 4 ),
 ( 0.000000000000000000, 0.0005385383678279382193, 0.001077076735655876439, 0.001615615103483814983, 0.001884884287397780786, 0.002154153471311746806 ),
 .UNSPECIFIED. ) ;
#4996=CARTESIAN_POINT ( 'NONE',  ( 1.748556056214748189, 1.384842366659678081, 0.1776433458945842758 ) ) ;
#5005=CARTESIAN_POINT ( 'NONE',  ( 1.556400554713971651, 1.293514327272109687, 0.2500000000000000000 ) ) ;
#5010=CARTESIAN_POINT ( 'NONE',  ( 1.413441772008046993, 1.058152734179773402, -0.2027185361817280818 ) ) ;
#5013=ORIENTED_EDGE ( 'NONE', *, *, #1320, .F. ) ;
#5015=CARTESIAN_POINT ( 'NONE',  ( -1.050138139902704104, -0.7221301030214424266, 0.2500000000000000000 ) ) ;
#5017=FACE_BOUND ( 'NONE', #651, .T. ) ;
#5019=CARTESIAN_POINT ( 'NONE',  ( -1.479329383613507964, -3.808562985511015242, 0.2179999999999999993 ) ) ;
#5020=CARTESIAN_POINT ( 'NONE',  ( 1.763818185482656009, 1.565523235941175928, -0.07053674507809003236 ) ) ;
#5021=ORIENTED_EDGE ( 'NONE', *, *, #2611, .T. ) ;
#5025=ORIENTED_EDGE ( 'NONE', *, *, #8024, .F. ) ;
#5026=CARTESIAN_POINT ( 'NONE',  ( -0.6570132742846659379, -0.6068321365170168402, 0.03200000000000000067 ) ) ;
#5027=CARTESIAN_POINT ( 'NONE',  ( 1.370061665056169886, 1.067877247819581488, -0.1419528184087927580 ) ) ;
#5028=EDGE_CURVE ( 'NONE', #7063, #3946, #4085, .T. ) ;
#5033=FACE_OUTER_BOUND ( 'NONE', #3529, .T. ) ;
#5037=VECTOR ( 'NONE', #3832, 39.37007874015748143 ) ;
#5044=ORIENTED_EDGE ( 'NONE', *, *, #4142, .T. ) ;
#5045=CARTESIAN_POINT ( 'NONE',  ( 1.401772513120452590, 1.065994035405744000, -0.1940432220382501405 ) ) ;
#5046=CARTESIAN_POINT ( 'NONE',  ( -1.204376266962890796, -0.2040480809676099017, 0.2179999999999999993 ) ) ;
#5054=DIRECTION ( 'NONE',  ( -0.6157549048526801405, 0.7879377495398141029, 0.000000000000000000 ) ) ;
#5056=DIRECTION ( 'NONE',  ( 0.7879377495398139919, 0.6157549048526802515, 0.000000000000000000 ) ) ;
#5061=CARTESIAN_POINT ( 'NONE',  ( 1.846835003037430534, 1.498370261438588313, 0.000000000000000000 ) ) ;
#5065=CARTESIAN_POINT ( 'NONE',  ( 1.302790242782180918, 1.667167568704493341, -0.1039999999999998703 ) ) ;
#5067=VERTEX_POINT ( 'NONE', #7277 ) ;
#5076=DIRECTION ( 'NONE',  ( -0.8875604078987042733, 0.4606913525677314158, 0.000000000000000000 ) ) ;
#5077=FACE_OUTER_BOUND ( 'NONE', #5108, .T. ) ;
#5078=( BOUNDED_SURFACE ( )  B_SPLINE_SURFACE ( 3, 2, ( 
 ( #3071, #5576, #2488 ),
 ( #4996, #7497, #4392 ),
 ( #1461, #806, #4060 ),
 ( #5903, #3270, #3235 ),
 ( #5155, #4624, #7005 ),
 ( #5771, #1381, #152 ),
 ( #4670, #279, #6474 ),
 ( #5740, #3893, #2648 ),
 ( #115, #2603, #7654 ),
 ( #1995, #771, #858 ),
 ( #734, #5110, #6426 ),
 ( #2044, #4025, #6388 ) ),
 .UNSPECIFIED., .F., .F., .F. ) 
 B_SPLINE_SURFACE_WITH_KNOTS ( ( 4, 2, 2, 2, 2, 4 ),
 ( 3, 3 ),
 ( 0.000000000000000000, 0.001544928261805478872, 0.002317392392708218091, 0.003089856523610957743, 0.004634784785416436181, 0.006179713047221915487 ),
 ( 0.000000000000000000, 1.000000000000000000 ),
 .UNSPECIFIED. ) 
 GEOMETRIC_REPRESENTATION_ITEM ( )  RATIONAL_B_SPLINE_SURFACE ( (
 ( 1.000000000000000000, 0.9155198504386535818, 1.000000000000000000),
 ( 1.000000000000000000, 0.9168944082009078400, 1.000000000000000000),
 ( 1.000000000000000000, 0.9178671560080209346, 1.000000000000000000),
 ( 1.000000000000000000, 0.9187365197604502320, 1.000000000000000000),
 ( 1.000000000000000000, 0.9189277564247825270, 1.000000000000000000),
 ( 1.000000000000000000, 0.9191098244346022073, 1.000000000000000000),
 ( 1.000000000000000000, 0.9190999940100047505, 1.000000000000000000),
 ( 1.000000000000000000, 0.9187630860089786022, 1.000000000000000000),
 ( 1.000000000000000000, 0.9181369762995320594, 1.000000000000000000),
 ( 1.000000000000000000, 0.9161154912244834359, 1.000000000000000000),
 ( 1.000000000000000000, 0.9147129675017228179, 1.000000000000000000),
 ( 1.000000000000000000, 0.9129308725696879678, 1.000000000000000000) ) ) 
 REPRESENTATION_ITEM ( '' )  SURFACE ( )  );
#5082=ORIENTED_EDGE ( 'NONE', *, *, #4135, .F. ) ;
#5084=CARTESIAN_POINT ( 'NONE',  ( 1.571814533976804151, 1.273076930690908437, 0.2372021369714001904 ) ) ;
#5088=CARTESIAN_POINT ( 'NONE',  ( 1.748511227875505725, 1.384809732886316702, 0.1776755382265015892 ) ) ;
#5091=CARTESIAN_POINT ( 'NONE',  ( 1.492904096916551460, 1.856349440303736831, -0.001813861035895662039 ) ) ;
#5096=CYLINDRICAL_SURFACE ( 'NONE', #1893, 0.1250000000000000000 ) ;
#5098=DIRECTION ( 'NONE',  ( 0.6157549048526801405, -0.7879377495398139919, 0.000000000000000000 ) ) ;
#5099=CARTESIAN_POINT ( 'NONE',  ( -6.110602001756019419, -1.404684638105634820, 0.3125000000000000000 ) ) ;
#5101=ORIENTED_EDGE ( 'NONE', *, *, #576, .F. ) ;
#5107=CARTESIAN_POINT ( 'NONE',  ( 1.260018307975525387, 1.633742302984369177, 0.2179999999999999993 ) ) ;
#5108=EDGE_LOOP ( 'NONE', ( #3944, #3959, #5021, #6141, #2538 ) ) ;
#5110=CARTESIAN_POINT ( 'NONE',  ( 1.856253616992894262, 1.480980492019778438, 0.01345717186770836390 ) ) ;
#5114=CARTESIAN_POINT ( 'NONE',  ( 0.02822771919327313195, 0.03615965030275954117, 0.2500000000000000000 ) ) ;
#5117=DIRECTION ( 'NONE',  ( -0.000000000000000000, -0.000000000000000000, -1.000000000000000000 ) ) ;
#5121=ADVANCED_FACE ( 'NONE', ( #5606 ), #7963, .T. ) ;
#5123=EDGE_CURVE ( 'NONE', #3263, #5878, #3193, .T. ) ;
#5127=EDGE_LOOP ( 'NONE', ( #1410, #1346, #6685, #2622 ) ) ;
#5130=ORIENTED_EDGE ( 'NONE', *, *, #2995, .T. ) ;
#5142=ORIENTED_EDGE ( 'NONE', *, *, #3589, .F. ) ;
#5144=FACE_BOUND ( 'NONE', #4599, .T. ) ;
#5145=ORIENTED_EDGE ( 'NONE', *, *, #3825, .F. ) ;
#5146=FACE_OUTER_BOUND ( 'NONE', #3503, .T. ) ;
#5152=ORIENTED_EDGE ( 'NONE', *, *, #3825, .T. ) ;
#5155=CARTESIAN_POINT ( 'NONE',  ( 1.789066932586632630, 1.414966942634559466, 0.1362372702697500215 ) ) ;
#5156=CARTESIAN_POINT ( 'NONE',  ( 1.535636747860705142, 1.849488204198513008, -0.03991733052746020138 ) ) ;
#5159=CARTESIAN_POINT ( 'NONE',  ( -6.057578121783967262, -1.099253028489540318, 0.3125000000000000000 ) ) ;
#5160=CARTESIAN_POINT ( 'NONE',  ( -1.204376266962895459, -0.2040480809675923046, 0.2266184113588085858 ) ) ;
#5162=ORIENTED_EDGE ( 'NONE', *, *, #5250, .F. ) ;
#5163=CARTESIAN_POINT ( 'NONE',  ( 1.452776126472616669, 1.185506347939969674, 0.2257575757582501175 ) ) ;
#5167=LINE ( 'NONE', #7181, #4387 ) ;
#5168=DIRECTION ( 'NONE',  ( -0.6157549048526775870, 0.7879377495398161013, 0.000000000000000000 ) ) ;
#5169=AXIS2_PLACEMENT_3D ( 'NONE', #6915, #4948, #3803 ) ;
#5175=CARTESIAN_POINT ( 'NONE',  ( 1.707875797406683382, 1.356648808867406020, 0.1757958501031237908 ) ) ;
#5177=EDGE_CURVE ( 'NONE', #2760, #3428, #2146, .T. ) ;
#5178=ORIENTED_EDGE ( 'NONE', *, *, #231, .F. ) ;
#5179=DIRECTION ( 'NONE',  ( -0.6157549048526804736, 0.7879377495398138809, 0.000000000000000000 ) ) ;
#5180=ORIENTED_EDGE ( 'NONE', *, *, #2725, .F. ) ;
#5181=CARTESIAN_POINT ( 'NONE',  ( 0.000000000000000000, 0.000000000000000000, 0.2500000000000000000 ) ) ;
#5183=DIRECTION ( 'NONE',  ( -0.7879377495398156572, -0.6157549048526781421, -0.000000000000000000 ) ) ;
#5189=AXIS2_PLACEMENT_3D ( 'NONE', #4836, #1674, #6672 ) ;
#5192=ADVANCED_FACE ( 'NONE', ( #7402 ), #6602, .F. ) ;
#5193=VERTEX_POINT ( 'NONE', #6748 ) ;
#5194=DIRECTION ( 'NONE',  ( 0.6157549048526803626, -0.7879377495398141029, 0.000000000000000000 ) ) ;
#5197=CARTESIAN_POINT ( 'NONE',  ( 1.626707180952940757, 1.340852667824533828, 0.2408335960773365370 ) ) ;
#5198=CARTESIAN_POINT ( 'NONE',  ( 1.360014742459622283, 1.082108298560946924, -0.1573894072555728219 ) ) ;
#5199=CIRCLE ( 'NONE', #4414, 7.490657474112464520 ) ;
#5203=ORIENTED_EDGE ( 'NONE', *, *, #3688, .T. ) ;
#5205=AXIS2_PLACEMENT_3D ( 'NONE', #5065, #5098, #6865 ) ;
#5206=ORIENTED_EDGE ( 'NONE', *, *, #7231, .F. ) ;
#5207=CARTESIAN_POINT ( 'NONE',  ( 1.436243482636471613, 1.812070496725654012, 0.1571406716987245322 ) ) ;
#5211=DIRECTION ( 'NONE',  ( -0.1461403971093831466, -0.1142052990486720071, 0.9826495479070427308 ) ) ;
#5212=CIRCLE ( 'NONE', #1665, 6.962657474112426748 ) ;
#5213=AXIS2_PLACEMENT_3D ( 'NONE', #3293, #5840, #1403 ) ;
#5217=EDGE_CURVE ( 'NONE', #112, #225, #6539, .T. ) ;
#5218=B_SPLINE_CURVE_WITH_KNOTS ( 'NONE', 3,
 ( #2453, #1108, #2961, #3656, #4347, #4224, #7461, #2407, #5659, #1226 ),
 .UNSPECIFIED., .F., .F.,
 ( 4, 2, 2, 2, 4 ),
 ( 3.400456267939447610E-16, 0.001260256529112787184, 0.002520513058225234363, 0.003780769587337681759, 0.005041026116450128720 ),
 .UNSPECIFIED. ) ;
#5219=DIRECTION ( 'NONE',  ( 9.649454429013018880E-17, 7.540822732871182162E-17, 1.000000000000000000 ) ) ;
#5222=VERTEX_POINT ( 'NONE', #6266 ) ;
#5232=ORIENTED_EDGE ( 'NONE', *, *, #5992, .T. ) ;
#5235=ORIENTED_EDGE ( 'NONE', *, *, #1274, .F. ) ;
#5237=CARTESIAN_POINT ( 'NONE',  ( 0.1250000000000000000, 1.530808498934191509E-17, 0.000000000000000000 ) ) ;
#5239=CARTESIAN_POINT ( 'NONE',  ( 1.584487667996386184, 1.282940758005886028, 0.2375274927211854514 ) ) ;
#5240=CARTESIAN_POINT ( 'NONE',  ( -4.882388066182494768, 5.670153330992220297, -0.05999999999999999778 ) ) ;
#5243=ADVANCED_FACE ( 'NONE', ( #2510, #5017 ), #7518, .F. ) ;
#5245=CARTESIAN_POINT ( 'NONE',  ( 0.8923633780935225079, 0.7607014108325282908, 0.2500000000000000000 ) ) ;
#5249=CARTESIAN_POINT ( 'NONE',  ( 1.514313407472767103, 1.834334088849169486, 0.06856807959217657567 ) ) ;
#5250=EDGE_CURVE ( 'NONE', #6429, #1576, #714, .T. ) ;
#5258=DIRECTION ( 'NONE',  ( -0.6568496200222102566, 0.7540216022612866720, -0.000000000000000000 ) ) ;
#5265=CARTESIAN_POINT ( 'NONE',  ( 1.469438155933634249, 1.205893913485946767, 0.2500000000000000555 ) ) ;
#5271=DIRECTION ( 'NONE',  ( 1.000000000000000000, 0.000000000000000000, 0.000000000000000000 ) ) ;
#5272=CARTESIAN_POINT ( 'NONE',  ( 1.780616048947831098, 1.055727875058976251, -0.08212881570848259982 ) ) ;
#5273=ORIENTED_EDGE ( 'NONE', *, *, #336, .T. ) ;
#5275=ORIENTED_EDGE ( 'NONE', *, *, #7043, .F. ) ;
#5277=VERTEX_POINT ( 'NONE', #4452 ) ;
#5281=CARTESIAN_POINT ( 'NONE',  ( 1.699282386309489246, 1.352382324664254565, 0.2085298325956354282 ) ) ;
#5288=CARTESIAN_POINT ( 'NONE',  ( 1.458223839541642475, 1.829247631064747193, 0.1297679841924749000 ) ) ;
#5289=DIRECTION ( 'NONE',  ( -0.6157549048526804736, 0.7879377495398138809, -0.000000000000000000 ) ) ;
#5291=CARTESIAN_POINT ( 'NONE',  ( 1.780616048947831986, 1.055727875058976917, -0.1039999999999998703 ) ) ;
#5295=ADVANCED_FACE ( 'NONE', ( #101 ), #5096, .F. ) ;
#5300=CARTESIAN_POINT ( 'NONE',  ( 1.536996473476847536, 1.850194254987160836, -0.04789697820785929205 ) ) ;
#5302=ORIENTED_EDGE ( 'NONE', *, *, #1581, .T. ) ;
#5307=CARTESIAN_POINT ( 'NONE',  ( 1.487965390510427088, 1.244492490061562817, 0.2500000000000000000 ) ) ;
#5309=ADVANCED_FACE ( 'NONE', ( #5679 ), #7597, .F. ) ;
#5314=VERTEX_POINT ( 'NONE', #3255 ) ;
#5315=CYLINDRICAL_SURFACE ( 'NONE', #6078, 0.03200000000000008393 ) ;
#5319=EDGE_LOOP ( 'NONE', ( #2274, #5429 ) ) ;
#5320=ORIENTED_EDGE ( 'NONE', *, *, #6921, .F. ) ;
#5322=VECTOR ( 'NONE', #4811, 39.37007874015748143 ) ;
#5324=CARTESIAN_POINT ( 'NONE',  ( 1.355995127727091409, 1.749358286058404488, 0.2179999999999997218 ) ) ;
#5330=TOROIDAL_SURFACE ( 'NONE', #354, 0.2704878104020024265, 0.03200000000000000067 ) ;
#5332=CARTESIAN_POINT ( 'NONE',  ( 1.260018307975524943, 1.633742302984368733, 0.2499999999999998890 ) ) ;
#5345=ORIENTED_EDGE ( 'NONE', *, *, #3179, .F. ) ;
#5347=CARTESIAN_POINT ( 'NONE',  ( 1.533242936008017532, 1.243109892254450344, 0.2356317254196890199 ) ) ;
#5349=EDGE_CURVE ( 'NONE', #4985, #5803, #3641, .T. ) ;
#5354=EDGE_CURVE ( 'NONE', #810, #7906, #6525, .T. ) ;
#5358=CARTESIAN_POINT ( 'NONE',  ( 0.009770039481058666320, -0.4636495502210370989, 0.2461822072133919292 ) ) ;
#5361=DIRECTION ( 'NONE',  ( -0.7879377495407453580, -0.6157549048514884271, 0.000000000000000000 ) ) ;
#5364=DIRECTION ( 'NONE',  ( 0.000000000000000000, 0.000000000000000000, -1.000000000000000000 ) ) ;
#5368=CARTESIAN_POINT ( 'NONE',  ( 1.635022706329736897, 1.287156158165765563, 0.2002339888563465509 ) ) ;
#5371=CARTESIAN_POINT ( 'NONE',  ( -4.882388066182508091, 5.670153330992292240, 0.2500000000000000000 ) ) ;
#5372=CARTESIAN_POINT ( 'NONE',  ( 1.537918127343594454, 1.852987194258524983, 0.000000000000000000 ) ) ;
#5373=DIRECTION ( 'NONE',  ( 0.000000000000000000, 0.000000000000000000, -1.000000000000000000 ) ) ;
#5386=EDGE_CURVE ( 'NONE', #3782, #4623, #2120, .T. ) ;
#5388=CARTESIAN_POINT ( 'NONE',  ( -1.047748016704662666, -0.7301584672333364390, 0.0008302559380426106136 ) ) ;
#5393=DIRECTION ( 'NONE',  ( -0.6157549048526804736, 0.7879377495398138809, 0.000000000000000000 ) ) ;
#5405=CYLINDRICAL_SURFACE ( 'NONE', #4008, 0.3243589946935200308 ) ;
#5412=CARTESIAN_POINT ( 'NONE',  ( -1.197351689389629881, -0.2276434618412936095, 0.0008144248133129071551 ) ) ;
#5413=CARTESIAN_POINT ( 'NONE',  ( 1.490392939745680323, 1.854387029763408190, -0.03263051443878305091 ) ) ;
#5415=VERTEX_POINT ( 'NONE', #4044 ) ;
#5416=DIRECTION ( 'NONE',  ( 0.6157549048526775870, -0.7879377495398161013, 0.000000000000000000 ) ) ;
#5419=CIRCLE ( 'NONE', #3215, 0.03200000000000002148 ) ;
#5420=CIRCLE ( 'NONE', #705, 0.03200000000000009781 ) ;
#5421=ORIENTED_EDGE ( 'NONE', *, *, #3589, .T. ) ;
#5425=CIRCLE ( 'NONE', #1895, 4.032000000000000917 ) ;
#5426=CARTESIAN_POINT ( 'NONE',  ( 0.3566525292043913886, -0.3408511508279085667, 0.2179999999999999993 ) ) ;
#5429=ORIENTED_EDGE ( 'NONE', *, *, #4938, .F. ) ;
#5435=CARTESIAN_POINT ( 'NONE',  ( 1.843369769566449712, 1.222798067273466627, -0.1039999999999998703 ) ) ;
#5437=CIRCLE ( 'NONE', #2294, 0.3099999999999745737 ) ;
#5440=CARTESIAN_POINT ( 'NONE',  ( 1.506219191374974731, 1.199057446088450440, 0.1758031223993888059 ) ) ;
#5441=DIRECTION ( 'NONE',  ( 1.000000000000000000, 0.000000000000000000, 0.000000000000000000 ) ) ;
#5444=ORIENTED_EDGE ( 'NONE', *, *, #7440, .F. ) ;
#5447=DIRECTION ( 'NONE',  ( -0.2323175946639496336, 0.9726399823210830631, 0.000000000000000000 ) ) ;
#5451=ORIENTED_EDGE ( 'NONE', *, *, #1569, .F. ) ;
#5458=ORIENTED_EDGE ( 'NONE', *, *, #7041, .T. ) ;
#5468=FACE_OUTER_BOUND ( 'NONE', #5763, .T. ) ;
#5469=CARTESIAN_POINT ( 'NONE',  ( 0.1015201953414744812, -0.4584396209566467539, 0.2207432131843653500 ) ) ;
#5471=CARTESIAN_POINT ( 'NONE',  ( 1.339249842318065653, 1.071711091725345621, -0.1040000000000607383 ) ) ;
#5473=ORIENTED_EDGE ( 'NONE', *, *, #2989, .T. ) ;
#5475=CARTESIAN_POINT ( 'NONE',  ( 0.08203198930727191585, -0.4609712184472686824, 0.02019114796704784762 ) ) ;
#5486=ADVANCED_FACE ( 'NONE', ( #1008 ), #2755, .T. ) ;
#5488=EDGE_CURVE ( 'NONE', #5193, #4706, #3505, .T. ) ;
#5492=CARTESIAN_POINT ( 'NONE',  ( 1.680017506572348163, 1.266475429936566144, 0.1957466405106247642 ) ) ;
#5494=ADVANCED_FACE ( 'NONE', ( #4692 ), #2829, .T. ) ;
#5495=CARTESIAN_POINT ( 'NONE',  ( 1.082008577329273136, 0.9412886604514951738, 0.03200000000000000067 ) ) ;
#5501=ORIENTED_EDGE ( 'NONE', *, *, #6150, .T. ) ;
#5502=CARTESIAN_POINT ( 'NONE',  ( 1.711017591405700422, 1.387320617706969461, 0.2054045915613178508 ) ) ;
#5515=CARTESIAN_POINT ( 'NONE',  ( 1.754394837573727051, 1.324599572866255848, 0.1638240367497202088 ) ) ;
#5516=CARTESIAN_POINT ( 'NONE',  ( 1.647496491878244429, 1.712196251980273365, -0.06032347067126962725 ) ) ;
#5517=ORIENTED_EDGE ( 'NONE', *, *, #2429, .F. ) ;
#5518=CARTESIAN_POINT ( 'NONE',  ( 1.624003765053596116, 1.278431772831593261, 0.2011290015196109116 ) ) ;
#5521=DIRECTION ( 'NONE',  ( -1.000000000000000000, 0.000000000000000000, 0.000000000000000000 ) ) ;
#5526=FACE_OUTER_BOUND ( 'NONE', #4817, .T. ) ;
#5527=VECTOR ( 'NONE', #3771, 39.37007874015748143 ) ;
#5528=ADVANCED_FACE ( 'NONE', ( #1533 ), #4165, .F. ) ;
#5538=CARTESIAN_POINT ( 'NONE',  ( 1.803445950851875201, 1.337549153712537464, 0.2500000000004169443 ) ) ;
#5539=EDGE_CURVE ( 'NONE', #5954, #6908, #7354, .T. ) ;
#5540=EDGE_CURVE ( 'NONE', #1576, #3501, #803, .T. ) ;
#5546=CARTESIAN_POINT ( 'NONE',  ( -0.5950975756886834889, 0.1840126700235211188, 0.03200000000000000067 ) ) ;
#5549=DIRECTION ( 'NONE',  ( 0.7879377495398138809, 0.6157549048526804736, 0.000000000000000000 ) ) ;
#5552=B_SPLINE_CURVE_WITH_KNOTS ( 'NONE', 3,
 ( #6700, #1087, #1128, #4976, #2973, #1740, #1821, #3136 ),
 .UNSPECIFIED., .F., .F.,
 ( 4, 2, 2, 4 ),
 ( 6.554322722250637004E-16, 0.001190714077523056602, 0.001786071116284258234, 0.002381428155045459648 ),
 .UNSPECIFIED. ) ;
#5554=ORIENTED_EDGE ( 'NONE', *, *, #426, .F. ) ;
#5557=CARTESIAN_POINT ( 'NONE',  ( 0.09357815549526610210, -0.4595590400308178780, 0.02446392532630315905 ) ) ;
#5558=MECHANICAL_CONTEXT ( 'NONE', #4207, 'mechanical' ) ;
#5559=CARTESIAN_POINT ( 'NONE',  ( 1.877707900143042563, 1.420965844381539167, -0.06059890939898970180 ) ) ;
#5561=VERTEX_POINT ( 'NONE', #7182 ) ;
#5564=AXIS2_PLACEMENT_3D ( 'NONE', #6135, #2348, #5638 ) ;
#5565=B_SPLINE_CURVE_WITH_KNOTS ( 'NONE', 3,
 ( #2228, #4723, #1609, #4114, #380, #7865, #4770, #6657 ),
 .UNSPECIFIED., .F., .F.,
 ( 4, 2, 2, 4 ),
 ( 0.0003409113597368014937, 0.001278283151453492609, 0.001746969047311835348, 0.002215654943170178304 ),
 .UNSPECIFIED. ) ;
#5569=CARTESIAN_POINT ( 'NONE',  ( 1.496213642433631197, 1.858935772646855611, -0.1039999999999998703 ) ) ;
#5571=VERTEX_POINT ( 'NONE', #368 ) ;
#5576=CARTESIAN_POINT ( 'NONE',  ( 1.731490805948541212, 1.384744806418967356, 0.1971537411642678150 ) ) ;
#5580=ORIENTED_EDGE ( 'NONE', *, *, #6552, .F. ) ;
#5581=DIRECTION ( 'NONE',  ( 0.7879377495398141029, 0.6157549048526802515, 0.000000000000000000 ) ) ;
#5582=DIRECTION ( 'NONE',  ( -0.6157549048526803626, 0.7879377495398141029, -0.000000000000000000 ) ) ;
#5584=VECTOR ( 'NONE', #4582, 39.37007874015748143 ) ;
#5587=ORIENTED_EDGE ( 'NONE', *, *, #732, .T. ) ;
#5590=CARTESIAN_POINT ( 'NONE',  ( 1.800863856793468276, 1.423917841411510343, 0.1209648279927613007 ) ) ;
#5591=DIRECTION ( 'NONE',  ( 0.7879377495398222075, 0.6157549048526698154, 0.000000000000000000 ) ) ;
#5593=EDGE_CURVE ( 'NONE', #3711, #5193, #4033, .T. ) ;
#5597=AXIS2_PLACEMENT_3D ( 'NONE', #498, #1, #659 ) ;
#5599=ADVANCED_FACE ( 'NONE', ( #7898 ), #1454, .T. ) ;
#5601=EDGE_LOOP ( 'NONE', ( #717, #6259, #7044, #5580, #5302 ) ) ;
#5603=DIRECTION ( 'NONE',  ( -0.000000000000000000, -0.000000000000000000, -1.000000000000000000 ) ) ;
#5605=CIRCLE ( 'NONE', #4164, 0.03200000000000007699 ) ;
#5606=FACE_OUTER_BOUND ( 'NONE', #6507, .T. ) ;
#5610=CARTESIAN_POINT ( 'NONE',  ( 1.597024068692529220, 1.785137331457983700, -2.037143834727303156E-14 ) ) ;
#5615=CARTESIAN_POINT ( 'NONE',  ( 1.271405812440770999, 1.084215362033057017, -0.08402758940906858431 ) ) ;
#5625=CARTESIAN_POINT ( 'NONE',  ( -1.194903880989551359, -0.2358655892081394090, 0.2500000000000000000 ) ) ;
#5629=CARTESIAN_POINT ( 'NONE',  ( 1.788798563727062474, 1.414764706470791333, 0.1365599753587105336 ) ) ;
#5635=EDGE_CURVE ( 'NONE', #1079, #5277, #3901, .T. ) ;
#5638=DIRECTION ( 'NONE',  ( -0.7879377495398141029, -0.6157549048526801405, 0.000000000000000000 ) ) ;
#5640=CARTESIAN_POINT ( 'NONE',  ( -0.01466378298870799936, -0.4621478854113529322, 0.0009103679542912866511 ) ) ;
#5643=CARTESIAN_POINT ( 'NONE',  ( 1.762538566111710558, 1.560058259527964619, -0.03170243290436908223 ) ) ;
#5648=ORIENTED_EDGE ( 'NONE', *, *, #7629, .F. ) ;
#5652=CARTESIAN_POINT ( 'NONE',  ( 0.02822771919327313195, 0.03615965030275954117, 0.2500000000000000000 ) ) ;
#5655=CARTESIAN_POINT ( 'NONE',  ( 1.087752123103788326, 1.539732657782964864, -0.2121970708454803678 ) ) ;
#5656=ORIENTED_EDGE ( 'NONE', *, *, #2383, .F. ) ;
#5657=DIRECTION ( 'NONE',  ( -0.6157549048526802515, 0.7879377495398142139, -0.000000000000000000 ) ) ;
#5659=CARTESIAN_POINT ( 'NONE',  ( 1.584990804742211212, 1.283332362320874998, 0.2375404096856918168 ) ) ;
#5662=CARTESIAN_POINT ( 'NONE',  ( 1.345710376364902983, 1.085941737115722283, -0.1453092053285080509 ) ) ;
#5668=DIRECTION ( 'NONE',  ( 0.6157549048526801405, -0.7879377495398139919, 0.000000000000000000 ) ) ;
#5679=FACE_OUTER_BOUND ( 'NONE', #2959, .T. ) ;
#5681=CARTESIAN_POINT ( 'NONE',  ( -1.023858060246952029, -0.8104042351526981047, -0.05999999999999999778 ) ) ;
#5685=DIRECTION ( 'NONE',  ( -1.000000000000000000, 0.000000000000000000, 0.000000000000000000 ) ) ;
#5690=VECTOR ( 'NONE', #3374, 39.37007874015748143 ) ;
#5691=CARTESIAN_POINT ( 'NONE',  ( 1.738285998806500032, 1.406929468094443969, 0.1853310783740557410 ) ) ;
#5692=EDGE_CURVE ( 'NONE', #3041, #1125, #3511, .T. ) ;
#5693=ORIENTED_EDGE ( 'NONE', *, *, #4403, .T. ) ;
#5698=TOROIDAL_SURFACE ( 'NONE', #1635, 0.4070000000000000839, 0.03200000000000000067 ) ;
#5706=DIRECTION ( 'NONE',  ( -1.000000000000000000, 0.000000000000000000, 0.000000000000000000 ) ) ;
#5707=CARTESIAN_POINT ( 'NONE',  ( 1.723350842796532278, 1.129006085766179890, -0.1039999999999998703 ) ) ;
#5711=CARTESIAN_POINT ( 'NONE',  ( 0.9690125299525021996, 0.8529848947786565772, 0.2179999999999999993 ) ) ;
#5713=CARTESIAN_POINT ( 'NONE',  ( 1.411244833761398310, 1.056435878372752324, -0.1949596646313069837 ) ) ;
#5720=CARTESIAN_POINT ( 'NONE',  ( 0.000000000000000000, 0.000000000000000000, 0.000000000000000000 ) ) ;
#5722=CARTESIAN_POINT ( 'NONE',  ( 1.420352459187311345, 1.205696483155414001, 0.2500000000000000000 ) ) ;
#5724=CARTESIAN_POINT ( 'NONE',  ( 1.764573863409885313, 1.564560119641652092, -0.07057956653668050195 ) ) ;
#5727=CIRCLE ( 'NONE', #1392, 6.870657474112407570 ) ;
#5732=DIRECTION ( 'NONE',  ( -0.5901435170775125583, 0.000000000000000000, -0.8072983520677988745 ) ) ;
#5735=CARTESIAN_POINT ( 'NONE',  ( 1.403524466810122107, 1.061529367020492831, -0.1913948864930017091 ) ) ;
#5737=DIRECTION ( 'NONE',  ( -0.7879377495398141029, -0.6157549048526801405, 0.000000000000000000 ) ) ;
#5738=EDGE_CURVE ( 'NONE', #6563, #2698, #8058, .T. ) ;
#5739=EDGE_CURVE ( 'NONE', #4364, #3462, #5218, .T. ) ;
#5740=CARTESIAN_POINT ( 'NONE',  ( 1.823361563706781707, 1.441291881570038402, 0.08644244353395109937 ) ) ;
#5744=CARTESIAN_POINT ( 'NONE',  ( 1.512219939927767820, 1.830831974065061596, -0.05383208248537842133 ) ) ;
#5746=ORIENTED_EDGE ( 'NONE', *, *, #2084, .T. ) ;
#5748=CARTESIAN_POINT ( 'NONE',  ( -0.5950975756886835999, 0.1840126700235212853, 0.2500000000000000000 ) ) ;
#5750=CARTESIAN_POINT ( 'NONE',  ( 0.2976660692273699338, -0.3850326757561698954, 0.000000000000000000 ) ) ;
#5752=CARTESIAN_POINT ( 'NONE',  ( 1.723083782080649939, 1.395997476760423961, 0.1965221205739769994 ) ) ;
#5755=ORIENTED_EDGE ( 'NONE', *, *, #2383, .T. ) ;
#5763=EDGE_LOOP ( 'NONE', ( #5805, #1483 ) ) ;
#5766=CARTESIAN_POINT ( 'NONE',  ( 1.662633195254459739, 1.344068888399850392, 0.2328741875126813521 ) ) ;
#5771=CARTESIAN_POINT ( 'NONE',  ( 1.801196254061721680, 1.424171435408524644, 0.1205097783069856016 ) ) ;
#5777=ORIENTED_EDGE ( 'NONE', *, *, #5945, .F. ) ;
#5800=DIRECTION ( 'NONE',  ( 0.000000000000000000, 0.000000000000000000, 1.000000000000000000 ) ) ;
#5801=B_SPLINE_CURVE_WITH_KNOTS ( 'NONE', 3,
 ( #5091, #1351, #7671, #3823, #6324, #130, #7019, #1283 ),
 .UNSPECIFIED., .F., .F.,
 ( 4, 2, 2, 4 ),
 ( -7.741103271180475610E-06, 0.0006266493673793644076, 0.0009438446027046368475, 0.001261039838029909179 ),
 .UNSPECIFIED. ) ;
#5803=VERTEX_POINT ( 'NONE', #1151 ) ;
#5805=ORIENTED_EDGE ( 'NONE', *, *, #7588, .T. ) ;
#5806=CARTESIAN_POINT ( 'NONE',  ( 1.800320205903116921, 1.030513867073702183, -0.08212881570848259982 ) ) ;
#5807=EDGE_LOOP ( 'NONE', ( #5890, #4421, #134, #207 ) ) ;
#5813=CIRCLE ( 'NONE', #575, 6.870657474112407570 ) ;
#5814=CARTESIAN_POINT ( 'NONE',  ( 1.473794063193210269, 1.841415396333994314, 0.05205027013366145955 ) ) ;
#5818=DIRECTION ( 'NONE',  ( -0.000000000000000000, -0.000000000000000000, -1.000000000000000000 ) ) ;
#5819=CARTESIAN_POINT ( 'NONE',  ( 0.3095776802284428975, -0.3772299648020716600, 0.0005848437636013204509 ) ) ;
#5829=CIRCLE ( 'NONE', #8036, 0.03200000000000002148 ) ;
#5831=CARTESIAN_POINT ( 'NONE',  ( 1.877688265130482037, 1.420950500079102286, -0.07807135826935437950 ) ) ;
#5835=ORIENTED_EDGE ( 'NONE', *, *, #1275, .F. ) ;
#5836=ORIENTED_EDGE ( 'NONE', *, *, #4403, .F. ) ;
#5837=EDGE_CURVE ( 'NONE', #4081, #3263, #1149, .T. ) ;
#5840=DIRECTION ( 'NONE',  ( 0.6157549048526804736, -0.7879377495398138809, 0.000000000000000000 ) ) ;
#5842=DIRECTION ( 'NONE',  ( -0.6157549048526802515, 0.7879377495398141029, -0.000000000000000000 ) ) ;
#5843=DIRECTION ( 'NONE',  ( 0.6157549048526803626, -0.7879377495398141029, 0.000000000000000000 ) ) ;
#5849=EDGE_CURVE ( 'NONE', #2215, #4005, #7805, .T. ) ;
#5850=ORIENTED_EDGE ( 'NONE', *, *, #4192, .F. ) ;
#5852=DIRECTION ( 'NONE',  ( 0.7879377495398139919, 0.6157549048526803626, 0.000000000000000000 ) ) ;
#5855=CARTESIAN_POINT ( 'NONE',  ( 1.733157827470028112, 1.373632878362779808, 0.1887011865797219856 ) ) ;
#5857=VECTOR ( 'NONE', #1246, 39.37007874015748143 ) ;
#5860=DIRECTION ( 'NONE',  ( 0.000000000000000000, 0.000000000000000000, -1.000000000000000000 ) ) ;
#5863=CARTESIAN_POINT ( 'NONE',  ( 1.378799321363650021, 1.727438546637902084, 0.2203823860013673641 ) ) ;
#5864=CARTESIAN_POINT ( 'NONE',  ( -4.882388066182508091, 5.670153330992292240, 0.2179999999999999993 ) ) ;
#5870=LINE ( 'NONE', #4590, #7501 ) ;
#5872=CARTESIAN_POINT ( 'NONE',  ( 1.556400554713971651, 1.293514327272109687, 0.2500000000000000000 ) ) ;
#5874=ORIENTED_EDGE ( 'NONE', *, *, #5692, .T. ) ;
#5875=DIRECTION ( 'NONE',  ( 0.000000000000000000, 0.000000000000000000, 1.000000000000000000 ) ) ;
#5876=LINE ( 'NONE', #338, #4101 ) ;
#5878=VERTEX_POINT ( 'NONE', #4505 ) ;
#5879=( NAMED_UNIT ( * ) PLANE_ANGLE_UNIT ( ) SI_UNIT ( $, .RADIAN. ) );
#5885=ORIENTED_EDGE ( 'NONE', *, *, #6921, .T. ) ;
#5890=ORIENTED_EDGE ( 'NONE', *, *, #1029, .T. ) ;
#5892=ORIENTED_EDGE ( 'NONE', *, *, #7231, .T. ) ;
#5893=CARTESIAN_POINT ( 'NONE',  ( 1.723083782080680360, 1.395997476760427958, 0.1965221205739619004 ) ) ;
#5894=DIRECTION ( 'NONE',  ( 0.000000000000000000, 0.000000000000000000, -1.000000000000000000 ) ) ;
#5899=LINE ( 'NONE', #273, #6855 ) ;
#5903=CARTESIAN_POINT ( 'NONE',  ( 1.782722070967079242, 1.410194317043852896, 0.1437129662472861058 ) ) ;
#5907=EDGE_CURVE ( 'NONE', #4005, #3933, #4141, .T. ) ;
#5909=DIRECTION ( 'NONE',  ( 1.000000000000000000, 0.000000000000000000, 0.000000000000000000 ) ) ;
#5910=B_SPLINE_CURVE_WITH_KNOTS ( 'NONE', 3,
 ( #253, #3416, #6651, #3379, #3495, #4107, #5918, #3450, #337, #6570, #4644, #6608 ),
 .UNSPECIFIED., .F., .F.,
 ( 4, 2, 2, 2, 2, 4 ),
 ( 0.000000000000000000, 0.0002733787321186933171, 0.0005467574642373866341, 0.001093514928474772835, 0.001640272392712158927, 0.002187029856949545235 ),
 .UNSPECIFIED. ) ;
#5913=B_SPLINE_CURVE_WITH_KNOTS ( 'NONE', 3,
 ( #3631, #3011, #6212, #7437, #6169, #3747, #1197, #2502 ),
 .UNSPECIFIED., .F., .F.,
 ( 4, 2, 2, 4 ),
 ( 0.000000000000000000, 0.0003176055034687256867, 0.0006352110069374513734, 0.001270422013874900795 ),
 .UNSPECIFIED. ) ;
#5917=ORIENTED_EDGE ( 'NONE', *, *, #8024, .T. ) ;
#5918=CARTESIAN_POINT ( 'NONE',  ( 0.3374272540027891121, -0.3568315896303838608, 0.2412390547417079811 ) ) ;
#5926=CYLINDRICAL_SURFACE ( 'NONE', #7526, 0.03200000000000001454 ) ;
#5931=CARTESIAN_POINT ( 'NONE',  ( -1.222146065255383940, -0.1443597716867830172, 0.3125000000000000000 ) ) ;
#5940=DIRECTION ( 'NONE',  ( -1.000000000000000000, -1.762482576557733776E-15, 0.000000000000000000 ) ) ;
#5944=ORIENTED_EDGE ( 'NONE', *, *, #3338, .T. ) ;
#5945=EDGE_CURVE ( 'NONE', #3903, #7979, #2536, .T. ) ;
#5946=DIRECTION ( 'NONE',  ( 0.3151807705563068884, 0.2463063934922189724, -0.9165119979555036434 ) ) ;
#5949=AXIS2_PLACEMENT_3D ( 'NONE', #1500, #5194, #5852 ) ;
#5951=LINE ( 'NONE', #1473, #3464 ) ;
#5952=CARTESIAN_POINT ( 'NONE',  ( 1.518108166580419915, 1.876045830693510164, 0.0007282234754631174015 ) ) ;
#5954=VERTEX_POINT ( 'NONE', #3271 ) ;
#5956=CARTESIAN_POINT ( 'NONE',  ( 1.328121161265039207, 1.072473730611112064, -0.1194156274346386548 ) ) ;
#5964=CARTESIAN_POINT ( 'NONE',  ( 0.9887166869077879117, 0.8277708867933823988, 0.03199999999999999373 ) ) ;
#5965=DIRECTION ( 'NONE',  ( -0.7879377495398141029, -0.6157549048526801405, 0.000000000000000000 ) ) ;
#5968=ORIENTED_EDGE ( 'NONE', *, *, #428, .T. ) ;
#5969=AXIS2_PLACEMENT_3D ( 'NONE', #4046, #6548, #420 ) ;
#5972=VECTOR ( 'NONE', #4683, 39.37007874015747433 ) ;
#5982=ORIENTED_EDGE ( 'NONE', *, *, #4846, .T. ) ;
#5992=EDGE_CURVE ( 'NONE', #5067, #7187, #4824, .T. ) ;
#5997=CARTESIAN_POINT ( 'NONE',  ( 1.492768560906099662, 1.856243522084602304, -0.0006067816429719980484 ) ) ;
#5999=ORIENTED_EDGE ( 'NONE', *, *, #4180, .F. ) ;
#6000=DIRECTION ( 'NONE',  ( -0.6157549048526804736, 0.7879377495398138809, 0.000000000000000000 ) ) ;
#6002=CARTESIAN_POINT ( 'NONE',  ( 1.566033889679777413, 1.280741487518077371, 0.2500000000000000555 ) ) ;
#6007=ORIENTED_EDGE ( 'NONE', *, *, #5539, .T. ) ;
#6008=ORIENTED_EDGE ( 'NONE', *, *, #2989, .F. ) ;
#6009=DIRECTION ( 'NONE',  ( 0.7879377495398141029, 0.6157549048526802515, 0.000000000000000000 ) ) ;
#6010=CARTESIAN_POINT ( 'NONE',  ( 1.452776126471488682, 1.185506347943134475, 0.2257575757576623099 ) ) ;
#6015=CARTESIAN_POINT ( 'NONE',  ( 0.2796912674003787513, -4.528516545235624413, 0.2500000000000000000 ) ) ;
#6028=CARTESIAN_POINT ( 'NONE',  ( 1.142655413120957197, 0.6307864494084283180, 0.2179999999999999993 ) ) ;
#6038=ORIENTED_EDGE ( 'NONE', *, *, #4734, .F. ) ;
#6040=CARTESIAN_POINT ( 'NONE',  ( 1.380988422954957606, 1.174934410395800821, 0.2500000000000000000 ) ) ;
#6042=CARTESIAN_POINT ( 'NONE',  ( 0.9690125299525020885, 0.8529848947786566882, 0.000000000000000000 ) ) ;
#6043=EDGE_CURVE ( 'NONE', #3239, #3428, #2692, .T. ) ;
#6048=EDGE_CURVE ( 'NONE', #7906, #810, #7283, .T. ) ;
#6050=CARTESIAN_POINT ( 'NONE',  ( 0.1028096983035132889, -0.4582465879184300372, 0.03199999999999999373 ) ) ;
#6051=PLANE ( 'NONE',  #2401 ) ;
#6064=CARTESIAN_POINT ( 'NONE',  ( 0.8923633780935225079, 0.7607014108325281798, 0.000000000000000000 ) ) ;
#6070=FACE_OUTER_BOUND ( 'NONE', #4039, .T. ) ;
#6078=AXIS2_PLACEMENT_3D ( 'NONE', #7799, #6009, #7833 ) ;
#6085=CARTESIAN_POINT ( 'NONE',  ( 0.09078267040543826216, -0.4599203499726461364, 0.2266307369244480729 ) ) ;
#6088=ORIENTED_EDGE ( 'NONE', *, *, #2679, .T. ) ;
#6095=DIRECTION ( 'NONE',  ( -0.000000000000000000, -0.000000000000000000, -1.000000000000000000 ) ) ;
#6096=CARTESIAN_POINT ( 'NONE',  ( -6.057578121783967262, -1.099253028489540318, 0.3125000000000000000 ) ) ;
#6105=FACE_OUTER_BOUND ( 'NONE', #1739, .T. ) ;
#6107=FACE_OUTER_BOUND ( 'NONE', #3161, .T. ) ;
#6108=CIRCLE ( 'NONE', #7287, 0.03200000000000003536 ) ;
#6109=CARTESIAN_POINT ( 'NONE',  ( 0.3566525292043903339, -0.3408511508279103985, 0.2179999999999999993 ) ) ;
#6115=CARTESIAN_POINT ( 'NONE',  ( 1.846835003037430534, 1.498370261438588313, 0.03199999999999999373 ) ) ;
#6116=AXIS2_PLACEMENT_3D ( 'NONE', #7248, #322, #4097 ) ;
#6126=VECTOR ( 'NONE', #5842, 39.37007874015748854 ) ;
#6129=ORIENTED_EDGE ( 'NONE', *, *, #3990, .T. ) ;
#6130=CARTESIAN_POINT ( 'NONE',  ( 0.9887166869077879117, 0.8277708867933823988, 0.2500000000000000000 ) ) ;
#6135=CARTESIAN_POINT ( 'NONE',  ( 1.652539028737726179, 1.219618926967090289, -0.1039999999999998703 ) ) ;
#6136=CARTESIAN_POINT ( 'NONE',  ( 0.02822771919327313195, 0.03615965030275954117, 0.000000000000000000 ) ) ;
#6139=DIRECTION ( 'NONE',  ( -1.000000000000000000, 0.000000000000000000, 0.000000000000000000 ) ) ;
#6141=ORIENTED_EDGE ( 'NONE', *, *, #5837, .F. ) ;
#6142=CARTESIAN_POINT ( 'NONE',  ( 1.608451107215755904, 1.301813166848322822, 0.2376577216243210278 ) ) ;
#6143=EDGE_CURVE ( 'NONE', #4660, #5314, #478, .T. ) ;
#6145=ORIENTED_EDGE ( 'NONE', *, *, #7200, .F. ) ;
#6146=CARTESIAN_POINT ( 'NONE',  ( 1.515917799388286635, 1.833721764662388232, -0.1039999999999998703 ) ) ;
#6148=CARTESIAN_POINT ( 'NONE',  ( 1.283278058574945257, 1.059461569165262462, -0.07928749764790786470 ) ) ;
#6149=DIRECTION ( 'NONE',  ( 0.7879377495398141029, 0.6157549048526802515, 0.000000000000000000 ) ) ;
#6150=EDGE_CURVE ( 'NONE', #3851, #518, #1005, .T. ) ;
#6152=EDGE_CURVE ( 'NONE', #4276, #4081, #1524, .T. ) ;
#6153=CARTESIAN_POINT ( 'NONE',  ( 1.544745509581308296, 0.8307882251580827049, -0.08212881570848259982 ) ) ;
#6163=ORIENTED_EDGE ( 'NONE', *, *, #5217, .F. ) ;
#6166=DIRECTION ( 'NONE',  ( 0.6157549048526804736, -0.7879377495398138809, 0.000000000000000000 ) ) ;
#6169=CARTESIAN_POINT ( 'NONE',  ( -1.042831394347257357, -0.7466732791099464084, 0.2376747752564828120 ) ) ;
#6175=CARTESIAN_POINT ( 'NONE',  ( 0.1024500231158892299, -0.4583009483847821364, 0.03046749565051176320 ) ) ;
#6178=CARTESIAN_POINT ( 'NONE',  ( 1.658388808675685056, 1.714694511436468005, 1.938114344956973572E-14 ) ) ;
#6179=CARTESIAN_POINT ( 'NONE',  ( 1.591243317659689405, 1.252944055095702725, 0.2002330193986645301 ) ) ;
#6193=EDGE_CURVE ( 'NONE', #1300, #4722, #3774, .T. ) ;
#6194=FACE_OUTER_BOUND ( 'NONE', #4814, .T. ) ;
#6205=ADVANCED_FACE ( 'NONE', ( #1144 ), #557, .F. ) ;
#6209=CARTESIAN_POINT ( 'NONE',  ( 0.7938352818576230874, 1.310043527237014560, 0.03200000000000000067 ) ) ;
#6212=CARTESIAN_POINT ( 'NONE',  ( -1.041235186073524277, -0.7520349028915425116, 0.2263769898119324941 ) ) ;
#6214=EDGE_CURVE ( 'NONE', #5222, #1079, #7418, .T. ) ;
#6216=AXIS2_PLACEMENT_3D ( 'NONE', #7235, #5364, #3427 ) ;
#6224=CARTESIAN_POINT ( 'NONE',  ( 1.904163605026766071, 1.432560671222282922, -6.829619984160658046E-16 ) ) ;
#6226=CARTESIAN_POINT ( 'NONE',  ( 1.725603453493498973, 1.399212170159634283, 0.2321060441915416273 ) ) ;
#6231=CARTESIAN_POINT ( 'NONE',  ( 1.322797517748710572, 1.071418997054937261, -0.08446866672460882908 ) ) ;
#6232=CARTESIAN_POINT ( 'NONE',  ( 1.380988422954957606, 1.174934410395800821, 0.2500000000000000000 ) ) ;
#6236=TOROIDAL_SURFACE ( 'NONE', #7406, 0.1523203157102362704, 0.06250000000000000000 ) ;
#6239=CARTESIAN_POINT ( 'NONE',  ( -6.163625881728066247, -1.710116247721755522, 0.3125000000000000000 ) ) ;
#6240=CIRCLE ( 'NONE', #4528, 0.3045082206899650812 ) ;
#6242=VERTEX_POINT ( 'NONE', #5569 ) ;
#6248=CIRCLE ( 'NONE', #2837, 0.2148203157102362704 ) ;
#6251=VECTOR ( 'NONE', #2331, 39.37007874015748143 ) ;
#6254=CARTESIAN_POINT ( 'NONE',  ( 1.832324720607670709, 1.448415597588696313, 0.06912397827687367935 ) ) ;
#6258=DIRECTION ( 'NONE',  ( 0.6157549048526804736, -0.7879377495398138809, 0.000000000000000000 ) ) ;
#6259=ORIENTED_EDGE ( 'NONE', *, *, #3038, .T. ) ;
#6266=CARTESIAN_POINT ( 'NONE',  ( 1.605841161801687900, 0.8785330470578376350, -0.1039999999999998287 ) ) ;
#6274=CARTESIAN_POINT ( 'NONE',  ( 1.492904096916551460, 1.856349440303736831, -0.001813861035895662039 ) ) ;
#6276=DIRECTION ( 'NONE',  ( 0.7879377495398124376, 0.6157549048526823610, -1.469929246256068058E-15 ) ) ;
#6284=CARTESIAN_POINT ( 'NONE',  ( 1.260018307975525387, 1.633742302984368733, 0.2500000000000000000 ) ) ;
#6291=FACE_OUTER_BOUND ( 'NONE', #3383, .T. ) ;
#6297=DIRECTION ( 'NONE',  ( 0.7879377495398135478, 0.6157549048526808066, 5.326735490302674370E-15 ) ) ;
#6299=CARTESIAN_POINT ( 'NONE',  ( 0.1028096983035134554, -0.4582465879184299817, 0.03120238169111335530 ) ) ;
#6301=DIRECTION ( 'NONE',  ( 0.8875604078987033851, -0.4606913525677331367, 0.000000000000000000 ) ) ;
#6303=ADVANCED_FACE ( 'NONE', ( #1752 ), #3670, .T. ) ;
#6308=DIRECTION ( 'NONE',  ( 0.2323175946639494671, -0.9726399823210830631, 0.000000000000000000 ) ) ;
#6309=CARTESIAN_POINT ( 'NONE',  ( 1.362414746624861506, 1.071731237471605480, -0.1509691161079382282 ) ) ;
#6318=CARTESIAN_POINT ( 'NONE',  ( 1.272185993414492122, 1.083697202197649423, -0.08467303850119081710 ) ) ;
#6322=CARTESIAN_POINT ( 'NONE',  ( 1.762749485016304574, 1.395289003792431037, 0.1650921806306561712 ) ) ;
#6324=CARTESIAN_POINT ( 'NONE',  ( 1.524344036321053197, 1.862279377486306231, -0.0001440199302405391986 ) ) ;
#6327=ORIENTED_EDGE ( 'NONE', *, *, #336, .F. ) ;
#6333=CARTESIAN_POINT ( 'NONE',  ( 1.780616048947831986, 1.055727875058976917, -0.1039999999999998703 ) ) ;
#6338=CIRCLE ( 'NONE', #6731, 0.1000000000000000194 ) ;
#6343=DIRECTION ( 'NONE',  ( 0.7879377495398223186, 0.6157549048526698154, -0.000000000000000000 ) ) ;
#6346=AXIS2_PLACEMENT_3D ( 'NONE', #7056, #3172, #6534 ) ;
#6347=B_SPLINE_CURVE_WITH_KNOTS ( 'NONE', 3,
 ( #5713, #2500, #5010, #1280 ),
 .UNSPECIFIED., .F., .F.,
 ( 4, 4 ),
 ( 1.268750569348874822E-13, 0.0003138637853426452448 ),
 .UNSPECIFIED. ) ;
#6349=CYLINDRICAL_SURFACE ( 'NONE', #25, 0.1250000000000000000 ) ;
#6353=CARTESIAN_POINT ( 'NONE',  ( 1.101712734285305473, 0.9160746524681562253, -0.3750000000000000555 ) ) ;
#6355=ORIENTED_EDGE ( 'NONE', *, *, #6048, .T. ) ;
#6360=AXIS2_PLACEMENT_3D ( 'NONE', #1642, #2751, #2873 ) ;
#6364=CARTESIAN_POINT ( 'NONE',  ( 1.713931971700676904, 1.282147506509141444, 0.1862199900718168877 ) ) ;
#6368=ORIENTED_EDGE ( 'NONE', *, *, #829, .F. ) ;
#6372=DIRECTION ( 'NONE',  ( 0.7879377495398141029, 0.6157549048526802515, 0.000000000000000000 ) ) ;
#6379=AXIS2_PLACEMENT_3D ( 'NONE', #834, #218, #1973 ) ;
#6384=DIRECTION ( 'NONE',  ( 0.4606913525677329146, 0.8875604078987036072, -0.000000000000000000 ) ) ;
#6388=CARTESIAN_POINT ( 'NONE',  ( 1.851982333143841197, 1.496483025098417796, -0.007738958973838943288 ) ) ;
#6407=CARTESIAN_POINT ( 'NONE',  ( 1.693178775325104191, 1.269413987854449255, 0.1923610198617223266 ) ) ;
#6409=ORIENTED_EDGE ( 'NONE', *, *, #4953, .F. ) ;
#6410=CARTESIAN_POINT ( 'NONE',  ( 1.640223930642815242, 1.235377681955144746, -0.1039999999999998703 ) ) ;
#6413=PLANE ( 'NONE',  #4548 ) ;
#6416=EDGE_LOOP ( 'NONE', ( #4697, #4386, #5777, #5648 ) ) ;
#6418=ORIENTED_EDGE ( 'NONE', *, *, #438, .T. ) ;
#6419=CARTESIAN_POINT ( 'NONE',  ( -0.5950975756886834889, 0.1840126700235211188, 0.2179999999999999993 ) ) ;
#6426=CARTESIAN_POINT ( 'NONE',  ( 1.846917295141469628, 1.491596352740438336, 0.01361236970061216640 ) ) ;
#6429=VERTEX_POINT ( 'NONE', #3921 ) ;
#6430=CARTESIAN_POINT ( 'NONE',  ( 1.279420049761111233, 1.085869607567433892, -0.09058840186730054977 ) ) ;
#6431=PLANE ( 'NONE',  #6761 ) ;
#6440=ORIENTED_EDGE ( 'NONE', *, *, #7831, .T. ) ;
#6441=DIRECTION ( 'NONE',  ( -1.000000000000000000, 0.000000000000000000, 0.000000000000000000 ) ) ;
#6443=CARTESIAN_POINT ( 'NONE',  ( 1.417311200634858492, 1.162707465448240773, 0.2206888379057397043 ) ) ;
#6454=LINE ( 'NONE', #1947, #60 ) ;
#6461=ORIENTED_EDGE ( 'NONE', *, *, #1458, .F. ) ;
#6464=ORIENTED_EDGE ( 'NONE', *, *, #6193, .T. ) ;
#6471=DIRECTION ( 'NONE',  ( -0.6157549048526802515, 0.7879377495398142139, -0.000000000000000000 ) ) ;
#6474=CARTESIAN_POINT ( 'NONE',  ( 1.797977497908697764, 1.451469997631733344, 0.1179144137747096116 ) ) ;
#6479=CARTESIAN_POINT ( 'NONE',  ( 0.3426393240825695297, -0.3526608655151391991, 0.01152805889772838717 ) ) ;
#6481=DIRECTION ( 'NONE',  ( -0.9726399823210830631, -0.2323175946639496336, -0.000000000000000000 ) ) ;
#6482=AXIS2_PLACEMENT_3D ( 'NONE', #7517, #2094, #4032 ) ;
#6485=AXIS2_PLACEMENT_3D ( 'NONE', #5272, #4726, #4821 ) ;
#6488=TOROIDAL_SURFACE ( 'NONE', #2950, 6.962657474112426748, 0.03200000000000000067 ) ;
#6493=CARTESIAN_POINT ( 'NONE',  ( 1.655938099986013379, 1.304250990722249037, 0.1968515939248739743 ) ) ;
#6505=CIRCLE ( 'NONE', #7535, 0.2819999999999998619 ) ;
#6507=EDGE_LOOP ( 'NONE', ( #182, #1844, #6906, #7887, #2529 ) ) ;
#6508=AXIS2_PLACEMENT_3D ( 'NONE', #6353, #3197, #808 ) ;
#6509=ORIENTED_EDGE ( 'NONE', *, *, #781, .T. ) ;
#6514=ORIENTED_EDGE ( 'NONE', *, *, #5635, .T. ) ;
#6516=DIRECTION ( 'NONE',  ( -0.000000000000000000, -0.000000000000000000, -1.000000000000000000 ) ) ;
#6520=CARTESIAN_POINT ( 'NONE',  ( 1.597320645397854122, 1.292162771345663375, 0.2367737893327029053 ) ) ;
#6525=CIRCLE ( 'NONE', #2979, 0.2148203157102361871 ) ;
#6532=ORIENTED_EDGE ( 'NONE', *, *, #6551, .T. ) ;
#6533=CARTESIAN_POINT ( 'NONE',  ( 1.339249842318065653, 1.071711091725345621, -0.1040000000000607383 ) ) ;
#6534=DIRECTION ( 'NONE',  ( 1.000000000000000000, 2.841121913410833274E-14, 0.000000000000000000 ) ) ;
#6539=B_SPLINE_CURVE_WITH_KNOTS ( 'NONE', 3,
 ( #1824, #6299, #6175, #1861, #2472, #4862, #673, #5557, #8040, #5475, #1204, #1743, #4252, #4369, #592, #5640, #2436, #4945 ),
 .UNSPECIFIED., .F., .F.,
 ( 4, 2, 2, 2, 2, 2, 2, 2, 4 ),
 ( 0.000000000000000000, 5.948296474276362620E-05, 0.0001189659294855272524, 0.0002379318589710563479, 0.0004758637179421140511, 0.0009517274358842289696, 0.001903454871768459240, 0.002855182307652689294, 0.003806909743536920215 ),
 .UNSPECIFIED. ) ;
#6540=CARTESIAN_POINT ( 'NONE',  ( 1.488944392314652365, 1.220926469523529345, 0.2500000000000000000 ) ) ;
#6541=ORIENTED_EDGE ( 'NONE', *, *, #1668, .T. ) ;
#6546=CARTESIAN_POINT ( 'NONE',  ( 1.449725606734969752, 1.190739840093742563, 0.2500000000000000000 ) ) ;
#6548=DIRECTION ( 'NONE',  ( 0.6157549048526802515, -0.7879377495398142139, 0.000000000000000000 ) ) ;
#6551=EDGE_CURVE ( 'NONE', #1218, #3851, #5727, .T. ) ;
#6552=EDGE_CURVE ( 'NONE', #684, #4837, #3924, .T. ) ;
#6553=DIRECTION ( 'NONE',  ( 0.7879377495398135478, 0.6157549048526808066, 1.794268796733532573E-15 ) ) ;
#6555=LINE ( 'NONE', #4167, #6989 ) ;
#6562=CARTESIAN_POINT ( 'NONE',  ( 0.3495740218478449179, -0.3469141891495676200, 0.01729592239954550956 ) ) ;
#6563=VERTEX_POINT ( 'NONE', #7847 ) ;
#6567=CARTESIAN_POINT ( 'NONE',  ( 1.515881672266826685, 1.874305877512008722, -0.03993337778610878130 ) ) ;
#6570=CARTESIAN_POINT ( 'NONE',  ( 0.3095788249173507256, -0.3772292882094739341, 0.2494153240220254031 ) ) ;
#6584=CIRCLE ( 'NONE', #423, 0.1000000000000000472 ) ;
#6590=FACE_OUTER_BOUND ( 'NONE', #7330, .T. ) ;
#6594=FACE_OUTER_BOUND ( 'NONE', #1948, .T. ) ;
#6596=DIRECTION ( 'NONE',  ( -0.000000000000000000, -0.000000000000000000, 1.000000000000000000 ) ) ;
#6598=CARTESIAN_POINT ( 'NONE',  ( 0.8923633780935229520, 0.7607014108325300672, 0.2500000000000000000 ) ) ;
#6599=ORIENTED_EDGE ( 'NONE', *, *, #1328, .T. ) ;
#6602=TOROIDAL_SURFACE ( 'NONE', #4768, 0.4024878104020024328, 0.1000000000000000056 ) ;
#6604=DIRECTION ( 'NONE',  ( 1.000000000000000000, 0.000000000000000000, 0.000000000000000000 ) ) ;
#6605=CARTESIAN_POINT ( 'NONE',  ( 1.490941149118869546, 1.854815442554424543, -0.04324422884743918394 ) ) ;
#6608=CARTESIAN_POINT ( 'NONE',  ( 0.2976660692273690456, -0.3850326757561704505, 0.2500000000000000000 ) ) ;
#6611=VERTEX_POINT ( 'NONE', #5559 ) ;
#6614=VECTOR ( 'NONE', #3553, 39.37007874015748143 ) ;
#6617=DIRECTION ( 'NONE',  ( 0.000000000000000000, 0.000000000000000000, 1.000000000000000000 ) ) ;
#6618=CARTESIAN_POINT ( 'NONE',  ( -1.040997396242601791, -0.7528336330030668266, 0.02354365816211315479 ) ) ;
#6619=FACE_OUTER_BOUND ( 'NONE', #1093, .T. ) ;
#6621=AXIS2_PLACEMENT_3D ( 'NONE', #931, #2152, #3423 ) ;
#6624=AXIS2_PLACEMENT_3D ( 'NONE', #7465, #2341, #2299 ) ;
#6644=CARTESIAN_POINT ( 'NONE',  ( -1.194903880989551359, -0.2358655892081394090, 0.000000000000000000 ) ) ;
#6646=CARTESIAN_POINT ( 'NONE',  ( 1.495180927969594009, 1.858128730468791678, 0.009522852913174784106 ) ) ;
#6650=DIRECTION ( 'NONE',  ( 0.000000000000000000, 0.000000000000000000, -1.000000000000000000 ) ) ;
#6651=CARTESIAN_POINT ( 'NONE',  ( 0.3553227796840386921, -0.3420127083024185333, 0.2250125263929970976 ) ) ;
#6652=CARTESIAN_POINT ( 'NONE',  ( 1.459523535701868324, 1.198274184545364829, 0.2499999999999795719 ) ) ;
#6656=EDGE_LOOP ( 'NONE', ( #2525, #2113, #7427, #4374, #7749, #5178, #4580, #3158, #3461, #274 ) ) ;
#6657=CARTESIAN_POINT ( 'NONE',  ( 1.859753234433174418, 1.471617347716406288, -0.009971652696953780398 ) ) ;
#6661=CARTESIAN_POINT ( 'NONE',  ( 1.640223930642815242, 1.235377681955144746, -0.1039999999999998703 ) ) ;
#6662=DIRECTION ( 'NONE',  ( -0.6157549048526801405, 0.7879377495398141029, 0.000000000000000000 ) ) ;
#6666=ORIENTED_EDGE ( 'NONE', *, *, #7351, .T. ) ;
#6669=VERTEX_POINT ( 'NONE', #5515 ) ;
#6670=DIRECTION ( 'NONE',  ( -1.000000000000000000, 0.000000000000000000, 0.000000000000000000 ) ) ;
#6672=DIRECTION ( 'NONE',  ( 1.000000000000000000, 3.824587191129967323E-15, 0.000000000000000000 ) ) ;
#6674=CYLINDRICAL_SURFACE ( 'NONE', #3714, 0.03200000000000008393 ) ;
#6675=CARTESIAN_POINT ( 'NONE',  ( 1.733157827470031220, 1.373632878362992527, 0.1887011865795288901 ) ) ;
#6680=DIRECTION ( 'NONE',  ( -0.000000000000000000, -0.000000000000000000, -1.000000000000000000 ) ) ;
#6682=ADVANCED_FACE ( 'NONE', ( #1703 ), #7553, .T. ) ;
#6685=ORIENTED_EDGE ( 'NONE', *, *, #3797, .F. ) ;
#6688=EDGE_CURVE ( 'NONE', #5803, #7906, #2571, .T. ) ;
#6692=CARTESIAN_POINT ( 'NONE',  ( 0.08210456126311437008, -0.4609633126210107013, 0.2297859553102247487 ) ) ;
#6700=CARTESIAN_POINT ( 'NONE',  ( 1.278468178840724834, 1.054204894366048473, -0.03540237177934978802 ) ) ;
#6703=( BOUNDED_SURFACE ( )  B_SPLINE_SURFACE ( 3, 2, ( 
 ( #3961, #725, #6955 ),
 ( #5239, #4016, #7604 ),
 ( #6520, #765, #185 ),
 ( #2685, #2767, #3306 ),
 ( #7074, #4541, #5197 ),
 ( #907, #5766, #3399 ),
 ( #2731, #3920, #7696 ),
 ( #5281, #4459, #1334 ),
 ( #2076, #1502, #4575 ),
 ( #1453, #3228, #2114 ),
 ( #849, #3842, #3355 ),
 ( #5855, #232, #5893 ) ),
 .UNSPECIFIED., .F., .F., .T. ) 
 B_SPLINE_SURFACE_WITH_KNOTS ( ( 4, 2, 2, 2, 2, 4 ),
 ( 3, 3 ),
 ( 0.000000000000000000, 0.001189084327048017331, 0.002378168654096034663, 0.003567252981144052211, 0.004161795144668060768, 0.004756337308192069326 ),
 ( 0.000000000000000000, 1.000000000000000000 ),
 .UNSPECIFIED. ) 
 GEOMETRIC_REPRESENTATION_ITEM ( )  RATIONAL_B_SPLINE_SURFACE ( (
 ( 1.000000000000000000, 0.8944458564818607016, 1.000000000000000000),
 ( 1.000000000000000000, 0.8965647441026000086, 1.000000000000000000),
 ( 1.000000000000000000, 0.8984366196282288497, 1.000000000000000000),
 ( 1.000000000000000000, 0.9019236665693611821, 1.000000000000000000),
 ( 1.000000000000000000, 0.9035407145860101519, 1.000000000000000000),
 ( 1.000000000000000000, 0.9068047609391414188, 1.000000000000000000),
 ( 1.000000000000000000, 0.9084452571090311235, 1.000000000000000000),
 ( 1.000000000000000000, 0.9110247302869100006, 1.000000000000000000),
 ( 1.000000000000000000, 0.9119054567922144638, 1.000000000000000000),
 ( 1.000000000000000000, 0.9137037716224694073, 1.000000000000000000),
 ( 1.000000000000000000, 0.9146239968701178613, 1.000000000000000000),
 ( 1.000000000000000000, 0.9155198504394047587, 1.000000000000000000) ) ) 
 REPRESENTATION_ITEM ( '' )  SURFACE ( )  );
#6706=ORIENTED_EDGE ( 'NONE', *, *, #5028, .F. ) ;
#6707=CIRCLE ( 'NONE', #3169, 0.2923589946935200579 ) ;
#6708=ORIENTED_EDGE ( 'NONE', *, *, #2372, .F. ) ;
#6709=CARTESIAN_POINT ( 'NONE',  ( 1.558885140107740819, 1.229058585821087179, 0.1943387615105033328 ) ) ;
#6715=DIRECTION ( 'NONE',  ( 1.000000000000000000, 0.000000000000000000, 0.000000000000000000 ) ) ;
#6716=DIRECTION ( 'NONE',  ( 0.7879377495398138809, 0.6157549048526804736, 0.000000000000000000 ) ) ;
#6720=VERTEX_POINT ( 'NONE', #1168 ) ;
#6721=CARTESIAN_POINT ( 'NONE',  ( 1.562204911103271421, 1.174407644688458818, 0.1842828921574816425 ) ) ;
#6731=AXIS2_PLACEMENT_3D ( 'NONE', #4516, #7017, #5685 ) ;
#6735=ORIENTED_EDGE ( 'NONE', *, *, #1578, .F. ) ;
#6748=CARTESIAN_POINT ( 'NONE',  ( 0.9207653111462810180, 0.7459592875503607834, 0.2179999999999999993 ) ) ;
#6751=DIRECTION ( 'NONE',  ( 0.7879377495398141029, 0.6157549048526802515, -0.000000000000000000 ) ) ;
#6753=CARTESIAN_POINT ( 'NONE',  ( 1.545700644469172547, 1.253231281308296863, 0.2367370325070441150 ) ) ;
#6761=AXIS2_PLACEMENT_3D ( 'NONE', #3974, #3441, #3481 ) ;
#6763=CARTESIAN_POINT ( 'NONE',  ( 1.754394837573727051, 1.324599572866255848, 0.1638240367497202088 ) ) ;
#6765=AXIS2_PLACEMENT_3D ( 'NONE', #4933, #6166, #538 ) ;
#6772=ORIENTED_EDGE ( 'NONE', *, *, #6988, .F. ) ;
#6774=TOROIDAL_SURFACE ( 'NONE', #4813, 4.032000000000000917, 0.03200000000000000067 ) ;
#6777=DIRECTION ( 'NONE',  ( -0.7879377495419734867, -0.6157549048499167954, 0.000000000000000000 ) ) ;
#6785=DIRECTION ( 'NONE',  ( -0.6157549048526801405, 0.7879377495398142139, 0.000000000000000000 ) ) ;
#6789=ORIENTED_EDGE ( 'NONE', *, *, #280, .F. ) ;
#6791=DIRECTION ( 'NONE',  ( 0.7879377495398141029, 0.6157549048526801405, 0.000000000000000000 ) ) ;
#6792=ADVANCED_FACE ( 'NONE', ( #4526 ), #3295, .T. ) ;
#6796=CARTESIAN_POINT ( 'NONE',  ( 1.315721141621744694, 1.089538881479228838, -0.1203794417438410480 ) ) ;
#6797=ADVANCED_FACE ( 'NONE', ( #4980 ), #6413, .F. ) ;
#6800=ORIENTED_EDGE ( 'NONE', *, *, #2982, .F. ) ;
#6801=PLANE ( 'NONE',  #2136 ) ;
#6805=EDGE_LOOP ( 'NONE', ( #1285, #7219, #1797, #3634 ) ) ;
#6806=PLANE ( 'NONE',  #5597 ) ;
#6823=CARTESIAN_POINT ( 'NONE',  ( 1.878103104100547593, 1.414113082497153728, -0.03271153132810599579 ) ) ;
#6830=EDGE_CURVE ( 'NONE', #140, #2070, #1015, .T. ) ;
#6835=CARTESIAN_POINT ( 'NONE',  ( 1.543631815526617546, 1.159893205310092101, 0.1758941433781722741 ) ) ;
#6847=DIRECTION ( 'NONE',  ( 0.7983857925064566929, 0.6021462665531003289, -0.000000000000000000 ) ) ;
#6849=CARTESIAN_POINT ( 'NONE',  ( 1.655521228349887242, 1.357097542742190743, 0.2318412895085913417 ) ) ;
#6853=CARTESIAN_POINT ( 'NONE',  ( 1.859753234433174418, 1.471617347716406288, -0.009971652696953780398 ) ) ;
#6855=VECTOR ( 'NONE', #2772, 39.37007874015748854 ) ;
#6858=AXIS2_PLACEMENT_3D ( 'NONE', #183, #62, #7037 ) ;
#6859=VERTEX_POINT ( 'NONE', #5681 ) ;
#6861=DIRECTION ( 'NONE',  ( -1.000000000000000000, 0.000000000000000000, 0.000000000000000000 ) ) ;
#6865=DIRECTION ( 'NONE',  ( 0.7879377495398141029, 0.6157549048526802515, 0.000000000000000000 ) ) ;
#6867=ORIENTED_EDGE ( 'NONE', *, *, #6552, .T. ) ;
#6871=CIRCLE ( 'NONE', #1504, 0.2923589946935200579 ) ;
#6873=ORIENTED_EDGE ( 'NONE', *, *, #90, .F. ) ;
#6875=CARTESIAN_POINT ( 'NONE',  ( 1.348222454147280480, 1.073204572620011898, -0.1377597263139525574 ) ) ;
#6879=CIRCLE ( 'NONE', #5969, 0.3024878104020024550 ) ;
#6881=ADVANCED_FACE ( 'NONE', ( #2594 ), #3766, .T. ) ;
#6888=CARTESIAN_POINT ( 'NONE',  ( 1.388198106678872445, 1.072068126535121069, -0.1818941674207988357 ) ) ;
#6889=CARTESIAN_POINT ( 'NONE',  ( -0.6148017326439689789, 0.2092266780087954636, 0.2500000000000000000 ) ) ;
#6894=ADVANCED_FACE ( 'NONE', ( #3257 ), #6774, .T. ) ;
#6906=ORIENTED_EDGE ( 'NONE', *, *, #4203, .F. ) ;
#6907=AXIS2_PLACEMENT_3D ( 'NONE', #1562, #4806, #332 ) ;
#6908=VERTEX_POINT ( 'NONE', #2022 ) ;
#6912=DIRECTION ( 'NONE',  ( -0.6157549048526804736, 0.7879377495398138809, 0.000000000000000000 ) ) ;
#6915=CARTESIAN_POINT ( 'NONE',  ( -6.110602001756019419, -1.404684638105634820, 0.3125000000000000000 ) ) ;
#6921=EDGE_CURVE ( 'NONE', #1342, #2815, #2055, .T. ) ;
#6931=EDGE_CURVE ( 'NONE', #5067, #6939, #788, .T. ) ;
#6933=CARTESIAN_POINT ( 'NONE',  ( -4.882388066182516084, 5.670153330992327767, 0.3125000000000000000 ) ) ;
#6939=VERTEX_POINT ( 'NONE', #7307 ) ;
#6941=ORIENTED_EDGE ( 'NONE', *, *, #4684, .F. ) ;
#6943=VERTEX_POINT ( 'NONE', #260 ) ;
#6950=DIRECTION ( 'NONE',  ( -0.000000000000000000, -0.000000000000000000, 1.000000000000000000 ) ) ;
#6951=EDGE_LOOP ( 'NONE', ( #6327, #266, #446, #2933 ) ) ;
#6954=ORIENTED_EDGE ( 'NONE', *, *, #6830, .T. ) ;
#6955=CARTESIAN_POINT ( 'NONE',  ( 1.556400554713971651, 1.293514327272109687, 0.2500000000000000000 ) ) ;
#6957=FACE_OUTER_BOUND ( 'NONE', #3471, .T. ) ;
#6967=DIRECTION ( 'NONE',  ( -0.6157549048526823610, 0.7879377495398123266, 0.000000000000000000 ) ) ;
#6969=ORIENTED_EDGE ( 'NONE', *, *, #1936, .T. ) ;
#6975=CARTESIAN_POINT ( 'NONE',  ( -4.882388066182494768, 5.670153330992220297, 0.3125000000000000000 ) ) ;
#6978=EDGE_LOOP ( 'NONE', ( #6145, #7295, #5836, #2267 ) ) ;
#6981=DIRECTION ( 'NONE',  ( 0.000000000000000000, 0.000000000000000000, 1.000000000000000000 ) ) ;
#6982=VECTOR ( 'NONE', #415, 39.37007874015748143 ) ;
#6988=EDGE_CURVE ( 'NONE', #7717, #3019, #98, .T. ) ;
#6989=VECTOR ( 'NONE', #937, 39.37007874015748143 ) ;
#6990=CIRCLE ( 'NONE', #6858, 0.03200000000000011169 ) ;
#6994=ORIENTED_EDGE ( 'NONE', *, *, #126, .T. ) ;
#6995=EDGE_CURVE ( 'NONE', #445, #3298, #4677, .T. ) ;
#6999=AXIS2_PLACEMENT_3D ( 'NONE', #4416, #5219, #7745 ) ;
#7001=CARTESIAN_POINT ( 'NONE',  ( 1.821876573136023136, 1.470292042915513520, 0.07759758242713811482 ) ) ;
#7005=CARTESIAN_POINT ( 'NONE',  ( 1.779809833619593773, 1.437619977954180950, 0.1424345704801376344 ) ) ;
#7010=CARTESIAN_POINT ( 'NONE',  ( -1.222146065255383940, -0.1443597716867830172, -0.05999999999999999778 ) ) ;
#7013=ORIENTED_EDGE ( 'NONE', *, *, #2134, .T. ) ;
#7017=DIRECTION ( 'NONE',  ( -0.000000000000000000, 0.000000000000000000, -1.000000000000000000 ) ) ;
#7018=AXIS2_PLACEMENT_3D ( 'NONE', #7487, #487, #6716 ) ;
#7019=CARTESIAN_POINT ( 'NONE',  ( 1.535166674676289089, 1.856143143388933492, -5.593666872230160467E-06 ) ) ;
#7020=CARTESIAN_POINT ( 'NONE',  ( 1.715112207380193654, 1.389698554653518103, 0.2327866256051912830 ) ) ;
#7021=TOROIDAL_SURFACE ( 'NONE', #3098, 0.1523203157102362704, 0.06250000000000000000 ) ;
#7024=ORIENTED_EDGE ( 'NONE', *, *, #2134, .F. ) ;
#7030=ORIENTED_EDGE ( 'NONE', *, *, #4142, .F. ) ;
#7032=ORIENTED_EDGE ( 'NONE', *, *, #5739, .T. ) ;
#7033=ORIENTED_EDGE ( 'NONE', *, *, #882, .T. ) ;
#7037=DIRECTION ( 'NONE',  ( -0.5035814659566155704, 0.8639477456102226949, 0.000000000000000000 ) ) ;
#7041=EDGE_CURVE ( 'NONE', #3041, #5878, #3342, .T. ) ;
#7042=CARTESIAN_POINT ( 'NONE',  ( -1.275477614966805673, 0.03477957369036089458, 0.2500000000000000000 ) ) ;
#7043=EDGE_CURVE ( 'NONE', #3946, #1218, #1641, .T. ) ;
#7044=ORIENTED_EDGE ( 'NONE', *, *, #781, .F. ) ;
#7049=CARTESIAN_POINT ( 'NONE',  ( 1.590963538254601684, 1.298412701918328915, -0.1039999999999998703 ) ) ;
#7051=ORIENTED_EDGE ( 'NONE', *, *, #528, .T. ) ;
#7056=CARTESIAN_POINT ( 'NONE',  ( 0.2796912674003787513, -4.528516545235624413, 0.03199999999999999373 ) ) ;
#7061=CARTESIAN_POINT ( 'NONE',  ( 1.452776126472616669, 1.185506347939969674, 0.2257575757582501175 ) ) ;
#7063=VERTEX_POINT ( 'NONE', #7108 ) ;
#7066=CARTESIAN_POINT ( 'NONE',  ( 0.9690125299525020885, 0.8529848947786566882, 0.03200000000000000067 ) ) ;
#7071=ORIENTED_EDGE ( 'NONE', *, *, #6043, .F. ) ;
#7073=ORIENTED_EDGE ( 'NONE', *, *, #2457, .F. ) ;
#7074=CARTESIAN_POINT ( 'NONE',  ( 1.637040878673387878, 1.317643376044983938, 0.2304635611191261646 ) ) ;
#7080=CARTESIAN_POINT ( 'NONE',  ( 1.386772069378664041, 1.773409745440035934, 0.2021634589242503610 ) ) ;
#7086=CARTESIAN_POINT ( 'NONE',  ( 0.3566525292043905560, -0.3408511508279104540, 0.02836266418265003669 ) ) ;
#7087=ORIENTED_EDGE ( 'NONE', *, *, #6043, .T. ) ;
#7092=ADVANCED_FACE ( 'NONE', ( #405 ), #6806, .F. ) ;
#7094=CARTESIAN_POINT ( 'NONE',  ( 1.494844024332783405, 1.818976347620703704, 0.1550510257216821397 ) ) ;
#7097=CARTESIAN_POINT ( 'NONE',  ( 1.490632003353124846, 1.854573852375907217, -0.03652564415615681959 ) ) ;
#7104=ORIENTED_EDGE ( 'NONE', *, *, #906, .F. ) ;
#7108=CARTESIAN_POINT ( 'NONE',  ( -1.023858060246952029, -0.8104042351526981047, 0.3125000000000000000 ) ) ;
#7113=EDGE_LOOP ( 'NONE', ( #2916, #7104, #6954, #917 ) ) ;
#7116=ORIENTED_EDGE ( 'NONE', *, *, #7440, .T. ) ;
#7124=ORIENTED_EDGE ( 'NONE', *, *, #438, .F. ) ;
#7125=CIRCLE ( 'NONE', #3724, 0.03200000000000000067 ) ;
#7129=FACE_OUTER_BOUND ( 'NONE', #5601, .T. ) ;
#7130=DIRECTION ( 'NONE',  ( -0.6157549048542445558, 0.7879377495385916363, 0.000000000000000000 ) ) ;
#7136=TOROIDAL_SURFACE ( 'NONE', #5564, 0.4024878104020024328, 0.1000000000000000056 ) ;
#7137=CARTESIAN_POINT ( 'NONE',  ( 1.421781027083512505, 1.064669666792219527, -0.2249973011472257700 ) ) ;
#7151=EDGE_CURVE ( 'NONE', #1559, #822, #3637, .T. ) ;
#7155=DIRECTION ( 'NONE',  ( 0.000000000000000000, 0.000000000000000000, -1.000000000000000000 ) ) ;
#7162=AXIS2_PLACEMENT_3D ( 'NONE', #5711, #93, #5168 ) ;
#7165=ORIENTED_EDGE ( 'NONE', *, *, #3403, .T. ) ;
#7166=DIRECTION ( 'NONE',  ( 0.000000000000000000, 0.000000000000000000, 1.000000000000000000 ) ) ;
#7172=DIRECTION ( 'NONE',  ( 0.000000000000000000, 0.000000000000000000, -1.000000000000000000 ) ) ;
#7177=CARTESIAN_POINT ( 'NONE',  ( 0.2976660692273699338, -0.3850326757561698954, 0.000000000000000000 ) ) ;
#7181=CARTESIAN_POINT ( 'NONE',  ( 1.854131197359395689, 1.310528858172997690, -0.1039999999999998703 ) ) ;
#7182=CARTESIAN_POINT ( 'NONE',  ( 1.611351012831676144, 0.9234512119983975253, -0.1039999999999998287 ) ) ;
#7184=VERTEX_POINT ( 'NONE', #6284 ) ;
#7187=VERTEX_POINT ( 'NONE', #2368 ) ;
#7194=CARTESIAN_POINT ( 'NONE',  ( -1.044522185028456063, -0.7409939553805848789, 0.006409361585647670688 ) ) ;
#7198=ORIENTED_EDGE ( 'NONE', *, *, #3797, .T. ) ;
#7200=EDGE_CURVE ( 'NONE', #6242, #2760, #1022, .T. ) ;
#7202=DIRECTION ( 'NONE',  ( -1.000000000000000000, 0.000000000000000000, 0.000000000000000000 ) ) ;
#7204=CARTESIAN_POINT ( 'NONE',  ( 1.846835003037430534, 1.498370261438588313, 0.000000000000000000 ) ) ;
#7205=ORIENTED_EDGE ( 'NONE', *, *, #6688, .F. ) ;
#7206=FACE_OUTER_BOUND ( 'NONE', #8053, .T. ) ;
#7208=LINE ( 'NONE', #6598, #1383 ) ;
#7219=ORIENTED_EDGE ( 'NONE', *, *, #2995, .F. ) ;
#7220=EDGE_LOOP ( 'NONE', ( #4939, #2394, #4911, #5232, #7355, #4080, #6418 ) ) ;
#7224=CARTESIAN_POINT ( 'NONE',  ( -1.040997396242601791, -0.7528336330030669377, 0.03199999999999999373 ) ) ;
#7228=ORIENTED_EDGE ( 'NONE', *, *, #6150, .F. ) ;
#7231=EDGE_CURVE ( 'NONE', #7797, #3462, #5605, .T. ) ;
#7235=CARTESIAN_POINT ( 'NONE',  ( -6.110602001756019419, -1.404684638105634820, 0.3125000000000000000 ) ) ;
#7243=EDGE_CURVE ( 'NONE', #6720, #5415, #1679, .T. ) ;
#7245=ORIENTED_EDGE ( 'NONE', *, *, #5488, .T. ) ;
#7248=CARTESIAN_POINT ( 'NONE',  ( 1.640223930642276118, 1.235377681956740803, -0.1039999999999998703 ) ) ;
#7251=CARTESIAN_POINT ( 'NONE',  ( 0.3566525292043903339, -0.3408511508279103985, 0.03199999999999999373 ) ) ;
#7252=ORIENTED_EDGE ( 'NONE', *, *, #4532, .F. ) ;
#7256=CARTESIAN_POINT ( 'NONE',  ( -1.203142842642319188, -0.2081911224984655251, 0.01565206492142497130 ) ) ;
#7257=CARTESIAN_POINT ( 'NONE',  ( 1.535356550020815947, 1.850327527696066898, -0.01560080253909610672 ) ) ;
#7263=DIRECTION ( 'NONE',  ( -0.9726399823210831741, -0.2323175946639494671, -0.000000000000000000 ) ) ;
#7265=LINE ( 'NONE', #4968, #3960 ) ;
#7277=CARTESIAN_POINT ( 'NONE',  ( 1.536996473475150671, 1.850194254988873244, -0.04789697820840163600 ) ) ;
#7280=CARTESIAN_POINT ( 'NONE',  ( -0.1250000000000000000, 0.000000000000000000, 0.000000000000000000 ) ) ;
#7283=CIRCLE ( 'NONE', #4022, 0.2148203157102361871 ) ;
#7284=VECTOR ( 'NONE', #2049, 39.37007874015748143 ) ;
#7286=CARTESIAN_POINT ( 'NONE',  ( 1.517943318015056109, 1.875917005398948456, 0.2500000000000000000 ) ) ;
#7287=AXIS2_PLACEMENT_3D ( 'NONE', #120, #2608, #6967 ) ;
#7289=AXIS2_PLACEMENT_3D ( 'NONE', #1203, #3588, #6861 ) ;
#7290=CYLINDRICAL_SURFACE ( 'NONE', #4517, 0.2500000000000000555 ) ;
#7292=ADVANCED_FACE ( 'NONE', ( #4629 ), #1465, .T. ) ;
#7295=ORIENTED_EDGE ( 'NONE', *, *, #4841, .T. ) ;
#7296=AXIS2_PLACEMENT_3D ( 'NONE', #5019, #3142, #6301 ) ;
#7297=CARTESIAN_POINT ( 'NONE',  ( 1.526053023712018897, 1.146155791044123573, 0.1638240367499944894 ) ) ;
#7300=EDGE_CURVE ( 'NONE', #1921, #4974, #5212, .T. ) ;
#7302=CARTESIAN_POINT ( 'NONE',  ( 1.082008577330675347, 0.9412886604525910750, -0.3750000000000000555 ) ) ;
#7306=ORIENTED_EDGE ( 'NONE', *, *, #1440, .F. ) ;
#7307=CARTESIAN_POINT ( 'NONE',  ( 1.877688265130482037, 1.420950500079102286, -0.07807135826935437950 ) ) ;
#7309=CARTESIAN_POINT ( 'NONE',  ( 1.477974616688189968, 1.237804197611785284, 0.2500000000000000000 ) ) ;
#7311=ORIENTED_EDGE ( 'NONE', *, *, #1186, .T. ) ;
#7317=DIRECTION ( 'NONE',  ( 0.9726399823210830631, 0.2323175946639496336, 0.000000000000000000 ) ) ;
#7320=CARTESIAN_POINT ( 'NONE',  ( -1.750746777110393282, 1.631196835986985505, 0.3125000000000000000 ) ) ;
#7324=CARTESIAN_POINT ( 'NONE',  ( 1.508496569261193576, 1.225487632694739037, 0.2349340013801235194 ) ) ;
#7327=CARTESIAN_POINT ( 'NONE',  ( 1.142655413120957197, 0.6307864494084283180, 0.2500000000000000000 ) ) ;
#7328=CARTESIAN_POINT ( 'NONE',  ( 0.000000000000000000, 0.000000000000000000, 0.2500000000000000000 ) ) ;
#7330=EDGE_LOOP ( 'NONE', ( #4651, #6008, #7702, #4266, #7228, #1034 ) ) ;
#7331=ORIENTED_EDGE ( 'NONE', *, *, #4684, .T. ) ;
#7332=CARTESIAN_POINT ( 'NONE',  ( -6.163625881728066247, -1.710116247721755522, -0.05999999999999999778 ) ) ;
#7343=ORIENTED_EDGE ( 'NONE', *, *, #126, .F. ) ;
#7347=CARTESIAN_POINT ( 'NONE',  ( 0.09365290641821995277, -0.4595491472197770766, 0.2255045796716246553 ) ) ;
#7351=EDGE_CURVE ( 'NONE', #5067, #3183, #3772, .T. ) ;
#7354=B_SPLINE_CURVE_WITH_KNOTS ( 'NONE', 3,
 ( #1695, #929, #2849, #5358, #2229, #4856, #2346, #1734, #6692, #6085, #7347, #464, #1075, #3579, #5469, #2967, #7956, #2293 ),
 .UNSPECIFIED., .F., .F.,
 ( 4, 2, 2, 2, 2, 2, 2, 2, 4 ),
 ( 0.000000000000000000, 0.0009393808714543294561, 0.001878761742908658912, 0.002818142614362988477, 0.003287833050090153367, 0.003522678267953735162, 0.003640100876885526276, 0.003698812181351423568, 0.003757523485817321294 ),
 .UNSPECIFIED. ) ;
#7355=ORIENTED_EDGE ( 'NONE', *, *, #3038, .F. ) ;
#7356=DIRECTION ( 'NONE',  ( 0.6157549048526804736, -0.7879377495398138809, -0.000000000000000000 ) ) ;
#7357=DIRECTION ( 'NONE',  ( -1.000000000000000000, 0.000000000000000000, 0.000000000000000000 ) ) ;
#7363=ORIENTED_EDGE ( 'NONE', *, *, #6988, .T. ) ;
#7365=DIRECTION ( 'NONE',  ( 9.649454429013021345E-17, 7.540822732871180930E-17, 1.000000000000000000 ) ) ;
#7368=CARTESIAN_POINT ( 'NONE',  ( 1.257489209309734290, 1.078422665367065658, -0.07268490389717283118 ) ) ;
#7373=CARTESIAN_POINT ( 'NONE',  ( 1.736793931975229688, 1.310844877195876279, 0.1759093273421855619 ) ) ;
#7374=AXIS2_PLACEMENT_3D ( 'NONE', #3599, #1056, #7929 ) ;
#7375=DIRECTION ( 'NONE',  ( 0.6157549048526802515, -0.7879377495398142139, 0.000000000000000000 ) ) ;
#7390=AXIS2_PLACEMENT_3D ( 'NONE', #6661, #5393, #6553 ) ;
#7395=EDGE_LOOP ( 'NONE', ( #7165, #2491, #7071, #999 ) ) ;
#7398=ORIENTED_EDGE ( 'NONE', *, *, #4846, .F. ) ;
#7399=EDGE_CURVE ( 'NONE', #7900, #3851, #2653, .T. ) ;
#7400=DIRECTION ( 'NONE',  ( 1.000000000000000000, 0.000000000000000000, 0.000000000000000000 ) ) ;
#7401=CARTESIAN_POINT ( 'NONE',  ( -4.882388066182516084, 5.670153330992327767, -0.05999999999999999778 ) ) ;
#7402=FACE_OUTER_BOUND ( 'NONE', #4171, .T. ) ;
#7406=AXIS2_PLACEMENT_3D ( 'NONE', #541, #6258, #5549 ) ;
#7408=CARTESIAN_POINT ( 'NONE',  ( 1.651395268467308108, 1.241511533269027634, 0.1986386654525169326 ) ) ;
#7410=CIRCLE ( 'NONE', #6624, 4.000000000000000888 ) ;
#7415=VERTEX_POINT ( 'NONE', #3317 ) ;
#7418=CIRCLE ( 'NONE', #7018, 0.2468203157102362155 ) ;
#7419=AXIS2_PLACEMENT_3D ( 'NONE', #1277, #7468, #8029 ) ;
#7420=DIRECTION ( 'NONE',  ( 0.7879377495398141029, 0.6157549048526801405, -9.106159978880875423E-16 ) ) ;
#7423=ORIENTED_EDGE ( 'NONE', *, *, #2982, .T. ) ;
#7426=DIRECTION ( 'NONE',  ( -1.000000000000000000, 0.000000000000000000, 0.000000000000000000 ) ) ;
#7427=ORIENTED_EDGE ( 'NONE', *, *, #7831, .F. ) ;
#7432=ORIENTED_EDGE ( 'NONE', *, *, #3824, .F. ) ;
#7437=CARTESIAN_POINT ( 'NONE',  ( -1.042152545007089648, -0.7489535171128813840, 0.2341260034930127132 ) ) ;
#7440=EDGE_CURVE ( 'NONE', #5561, #5277, #6248, .T. ) ;
#7441=EDGE_LOOP ( 'NONE', ( #6440, #1801, #4075, #8028, #3135, #6007, #962, #1847 ) ) ;
#7443=DIRECTION ( 'NONE',  ( 1.000000000000000000, 0.000000000000000000, 0.000000000000000000 ) ) ;
#7448=CARTESIAN_POINT ( 'NONE',  ( -0.03921911030312474900, -0.4592703903598064352, 0.000000000000000000 ) ) ;
#7449=CARTESIAN_POINT ( 'NONE',  ( 1.693003829518198389, 1.370386348581982050, 0.2342090033200751320 ) ) ;
#7451=ADVANCED_FACE ( 'NONE', ( #283 ), #3408, .F. ) ;
#7456=ORIENTED_EDGE ( 'NONE', *, *, #1274, .T. ) ;
#7458=LINE ( 'NONE', #6153, #7625 ) ;
#7461=CARTESIAN_POINT ( 'NONE',  ( 1.625764008135038186, 1.310881905705549189, 0.2328597852778326871 ) ) ;
#7464=CARTESIAN_POINT ( 'NONE',  ( 1.556400554713971651, 1.293514327272109687, 0.2179999999999999993 ) ) ;
#7465=CARTESIAN_POINT ( 'NONE',  ( 0.2796912674003787513, -4.528516545235624413, 0.2179999999999999993 ) ) ;
#7466=EDGE_LOOP ( 'NONE', ( #3965, #6994 ) ) ;
#7467=CARTESIAN_POINT ( 'NONE',  ( 1.626644885887612135, 1.340816597564956636, 0.2408507084050821034 ) ) ;
#7468=DIRECTION ( 'NONE',  ( 9.649454429013021345E-17, 7.540822732871180930E-17, 1.000000000000000000 ) ) ;
#7471=DIRECTION ( 'NONE',  ( 0.6157549048526806956, -0.7879377495398136588, 0.000000000000000000 ) ) ;
#7478=CARTESIAN_POINT ( 'NONE',  ( 0.1028096983035134415, -0.4582465879184300372, 0.03199999999999999373 ) ) ;
#7480=EDGE_CURVE ( 'NONE', #7825, #2232, #1138, .T. ) ;
#7487=CARTESIAN_POINT ( 'NONE',  ( 1.800320205903117809, 1.030513867073702627, -0.1039999999999998703 ) ) ;
#7493=ADVANCED_FACE ( 'NONE', ( #3165 ), #5330, .T. ) ;
#7497=CARTESIAN_POINT ( 'NONE',  ( 1.747147036660383401, 1.396167064578475392, 0.1856492696740475179 ) ) ;
#7501=VECTOR ( 'NONE', #6481, 39.37007874015748143 ) ;
#7503=LINE ( 'NONE', #6889, #2690 ) ;
#7505=CARTESIAN_POINT ( 'NONE',  ( 1.612291730907446929, 1.332246407104009212, 0.2442446905291179859 ) ) ;
#7512=AXIS2_PLACEMENT_3D ( 'NONE', #6146, #3022, #5521 ) ;
#7513=AXIS2_PLACEMENT_3D ( 'NONE', #481, #1749, #5441 ) ;
#7514=VECTOR ( 'NONE', #1944, 39.37007874015748854 ) ;
#7517=CARTESIAN_POINT ( 'NONE',  ( 1.827130846082144711, 1.523584269423862381, 0.03199999999999999373 ) ) ;
#7518=PLANE ( 'NONE',  #4897 ) ;
#7521=CARTESIAN_POINT ( 'NONE',  ( 1.645591831251460357, 1.707080862284764411, -0.02857125970228467995 ) ) ;
#7524=VECTOR ( 'NONE', #6095, 39.37007874015748143 ) ;
#7526=AXIS2_PLACEMENT_3D ( 'NONE', #2882, #7317, #7762 ) ;
#7531=CARTESIAN_POINT ( 'NONE',  ( 1.415867837616119340, 1.058804471812468062, -0.2073170131698808538 ) ) ;
#7532=CARTESIAN_POINT ( 'NONE',  ( 0.8923633780935220638, 0.7607014108325284019, 0.2179999999999999993 ) ) ;
#7535=AXIS2_PLACEMENT_3D ( 'NONE', #4069, #5875, #4717 ) ;
#7539=CARTESIAN_POINT ( 'NONE',  ( 1.640223930641419914, 1.235377681954054285, -0.08212881570848259982 ) ) ;
#7543=DIRECTION ( 'NONE',  ( -0.000000000000000000, -0.000000000000000000, -1.000000000000000000 ) ) ;
#7544=( BOUNDED_SURFACE ( )  B_SPLINE_SURFACE ( 3, 2, ( 
 ( #254, #6002, #3451 ),
 ( #3380, #7905, #2799 ),
 ( #2187, #4155, #5347 ),
 ( #5307, #7862, #1001 ),
 ( #7309, #6540, #7794 ),
 ( #7828, #5265, #1528 ),
 ( #4108, #6652, #3417 ),
 ( #4686, #1566, #4070 ) ),
 .UNSPECIFIED., .F., .F., .F. ) 
 B_SPLINE_SURFACE_WITH_KNOTS ( ( 4, 2, 2, 4 ),
 ( 3, 3 ),
 ( 0.000000000000000000, 0.001832226346958918360, 0.002748339520438377540, 0.003664452693917836720 ),
 ( 0.000000000000000000, 1.000000000000000000 ),
 .UNSPECIFIED. ) 
 GEOMETRIC_REPRESENTATION_ITEM ( )  RATIONAL_B_SPLINE_SURFACE ( (
 ( 1.000000000000000000, 0.8944458564818607016, 1.000000000000000000),
 ( 1.000000000000000000, 0.8900330376657383802, 1.000000000000000000),
 ( 1.000000000000000000, 0.8807711115184968520, 1.000000000000000000),
 ( 1.000000000000000000, 0.8564896213547265047, 1.000000000000000000),
 ( 1.000000000000000000, 0.8466679407797762513, 1.000000000000000000),
 ( 1.000000000000000000, 0.8220717958220354893, 1.000000000000000000),
 ( 1.000000000000000000, 0.8073589957100081316, 1.000000000000000000),
 ( 1.000000000000000000, 0.7881701093105710765, 1.000000000000000000) ) ) 
 REPRESENTATION_ITEM ( '' )  SURFACE ( )  );
#7547=CYLINDRICAL_SURFACE ( 'NONE', #3048, 0.2148203157102362704 ) ;
#7552=EDGE_LOOP ( 'NONE', ( #6509, #617, #6666, #6368 ) ) ;
#7553=TOROIDAL_SURFACE ( 'NONE', #1529, 0.4070000000000000839, 0.03200000000000000067 ) ;
#7556=DIRECTION ( 'NONE',  ( 0.2323175946639585154, -0.9726399823210809537, 0.000000000000000000 ) ) ;
#7557=DIRECTION ( 'NONE',  ( -0.7879377495398138809, -0.6157549048526803626, 0.000000000000000000 ) ) ;
#7560=VECTOR ( 'NONE', #7800, 39.37007874015748143 ) ;
#7561=ORIENTED_EDGE ( 'NONE', *, *, #5354, .T. ) ;
#7563=DIRECTION ( 'NONE',  ( -0.000000000000000000, -0.000000000000000000, -1.000000000000000000 ) ) ;
#7565=DIRECTION ( 'NONE',  ( 1.000000000000000000, 0.000000000000000000, 0.000000000000000000 ) ) ;
#7572=DIRECTION ( 'NONE',  ( 0.000000000000000000, 0.000000000000000000, 1.000000000000000000 ) ) ;
#7577=DIRECTION ( 'NONE',  ( -0.6157549048526801405, 0.7879377495398142139, 0.000000000000000000 ) ) ;
#7584=( BOUNDED_SURFACE ( )  B_SPLINE_SURFACE ( 3, 2, ( 
 ( #6224, #6823, #1134 ),
 ( #595, #3143, #1169 ),
 ( #1864, #5643, #5020 ),
 ( #4372, #1911, #1207 ),
 ( #6178, #7521, #5516 ),
 ( #5610, #3056, #3104 ),
 ( #4420, #2393, #4294 ),
 ( #7966, #3642, #8085 ) ),
 .UNSPECIFIED., .F., .F., .F. ) 
 B_SPLINE_SURFACE_WITH_KNOTS ( ( 4, 2, 2, 4 ),
 ( 3, 3 ),
 ( 0.01821389010018729937, 0.02536405575626812098, 0.02893913858430853178, 0.03251422141234894259 ),
 ( 0.000000000000000000, 1.000000000000000000 ),
 .UNSPECIFIED. ) 
 GEOMETRIC_REPRESENTATION_ITEM ( )  RATIONAL_B_SPLINE_SURFACE ( (
 ( 1.000000000000000000, 0.9094853233922192137, 1.000000000000000000),
 ( 1.000000000000000000, 0.9206922740272390770, 1.000000000000000000),
 ( 1.000000000000000000, 0.9314353586015322595, 1.000000000000000000),
 ( 1.000000000000000000, 0.9469214819804713246, 1.000000000000000000),
 ( 1.000000000000000000, 0.9519774771984306216, 1.000000000000000000),
 ( 1.000000000000000000, 0.9618860785231415633, 1.000000000000000000),
 ( 1.000000000000000000, 0.9667392787164085233, 1.000000000000000000),
 ( 1.000000000000000000, 0.9714909886463486410, 1.000000000000000000) ) ) 
 REPRESENTATION_ITEM ( '' )  SURFACE ( )  );
#7587=CARTESIAN_POINT ( 'NONE',  ( 0.3566525292043903339, -0.3408511508279103985, 0.03199999999999999373 ) ) ;
#7588=EDGE_CURVE ( 'NONE', #5803, #4985, #4932, .T. ) ;
#7590=ORIENTED_EDGE ( 'NONE', *, *, #7595, .T. ) ;
#7592=EDGE_CURVE ( 'NONE', #3346, #4364, #2166, .T. ) ;
#7594=PRODUCT_DEFINITION ( 'UNKNOWN', '', #1211, #2857 ) ;
#7595=EDGE_CURVE ( 'NONE', #6429, #3711, #4802, .T. ) ;
#7597=CYLINDRICAL_SURFACE ( 'NONE', #6379, 0.2148203157102362704 ) ;
#7604=CARTESIAN_POINT ( 'NONE',  ( 1.570147038066920908, 1.304011843337828491, 0.2500000000000000000 ) ) ;
#7605=CARTESIAN_POINT ( 'NONE',  ( 1.389858159471070609, 1.065857478577425521, -0.1776095199200875552 ) ) ;
#7606=DIRECTION ( 'NONE',  ( -1.000000000000000000, 0.000000000000000000, 0.000000000000000000 ) ) ;
#7613=ORIENTED_EDGE ( 'NONE', *, *, #829, .T. ) ;
#7615=DIRECTION ( 'NONE',  ( -0.000000000000000000, -0.000000000000000000, -1.000000000000000000 ) ) ;
#7624=CARTESIAN_POINT ( 'NONE',  ( 1.661823184001568698, 1.248966711494948312, 0.1978336168691578745 ) ) ;
#7625=VECTOR ( 'NONE', #4339, 39.37007874015748854 ) ;
#7629=EDGE_CURVE ( 'NONE', #6563, #3903, #5199, .T. ) ;
#7633=SHAPE_DEFINITION_REPRESENTATION ( #7861, #2505 ) ;
#7637=EDGE_LOOP ( 'NONE', ( #7650, #4711, #1802, #4298 ) ) ;
#7643=FACE_OUTER_BOUND ( 'NONE', #1228, .T. ) ;
#7650=ORIENTED_EDGE ( 'NONE', *, *, #428, .F. ) ;
#7654=CARTESIAN_POINT ( 'NONE',  ( 1.824088629755107549, 1.472086675550743129, 0.07316101119560965149 ) ) ;
#7657=EDGE_LOOP ( 'NONE', ( #555, #3762, #3876, #5693, #4596, #1968 ) ) ;
#7658=CARTESIAN_POINT ( 'NONE',  ( 1.244866787915867912, 1.068558539350931369, -0.06210292240210582571 ) ) ;
#7659=APPLICATION_CONTEXT ( 'configuration controlled 3d designs of mechanical parts and assemblies' ) ;
#7660=FACE_OUTER_BOUND ( 'NONE', #490, .T. ) ;
#7662=EDGE_LOOP ( 'NONE', ( #201, #5746, #5275, #6706 ) ) ;
#7664=LINE ( 'NONE', #2584, #3178 ) ;
#7665=CIRCLE ( 'NONE', #4138, 0.3243589946935200308 ) ;
#7671=CARTESIAN_POINT ( 'NONE',  ( 1.507878486496126325, 1.864120309560733046, -0.0006456303409778649856 ) ) ;
#7673=CARTESIAN_POINT ( 'NONE',  ( 1.666036690277059584, 1.312801532736543875, 0.1943274194496727170 ) ) ;
#7679=B_SPLINE_CURVE_WITH_KNOTS ( 'NONE', 3,
 ( #2932, #2320, #1704, #4255, #4328, #2475 ),
 .UNSPECIFIED., .F., .F.,
 ( 4, 2, 4 ),
 ( 0.000000000000000000, 0.001832226346962038694, 0.003664452693924077388 ),
 .UNSPECIFIED. ) ;
#7683=FACE_OUTER_BOUND ( 'NONE', #5127, .T. ) ;
#7686=ORIENTED_EDGE ( 'NONE', *, *, #3885, .T. ) ;
#7689=ORIENTED_EDGE ( 'NONE', *, *, #1538, .T. ) ;
#7694=CARTESIAN_POINT ( 'NONE',  ( 1.710665627987878468, 1.385179670250965778, 0.1690855662849976571 ) ) ;
#7695=EDGE_LOOP ( 'NONE', ( #1259, #2965, #1011, #2609 ) ) ;
#7696=CARTESIAN_POINT ( 'NONE',  ( 1.669937403698680045, 1.364736155589769462, 0.2262520360130875763 ) ) ;
#7697=CARTESIAN_POINT ( 'NONE',  ( 1.405770222897310129, 1.058238628546103843, -0.1877720200186123178 ) ) ;
#7702=ORIENTED_EDGE ( 'NONE', *, *, #7838, .F. ) ;
#7703=CARTESIAN_POINT ( 'NONE',  ( 1.455867074896413094, 1.788230745717717340, 0.1579256027718150546 ) ) ;
#7712=CYLINDRICAL_SURFACE ( 'NONE', #6482, 0.03200000000000003536 ) ;
#7717=VERTEX_POINT ( 'NONE', #5748 ) ;
#7729=ORIENTED_EDGE ( 'NONE', *, *, #906, .T. ) ;
#7732=CARTESIAN_POINT ( 'NONE',  ( 1.320852648564097009, 1.681729342627086732, 0.2439623838516123966 ) ) ;
#7737=CARTESIAN_POINT ( 'NONE',  ( 1.316445289774556660, 1.089505585486493455, -0.1209773538345980948 ) ) ;
#7742=CARTESIAN_POINT ( 'NONE',  ( 1.526053023712018897, 1.146155791044123573, 0.1638240367499944894 ) ) ;
#7745=DIRECTION ( 'NONE',  ( 1.000000000000000000, 0.000000000000000000, 0.000000000000000000 ) ) ;
#7746=CARTESIAN_POINT ( 'NONE',  ( 1.389292273488484053, 1.735715544542429933, 0.2499999999999999167 ) ) ;
#7749=ORIENTED_EDGE ( 'NONE', *, *, #1320, .T. ) ;
#7755=AXIS2_PLACEMENT_3D ( 'NONE', #866, #5946, #325 ) ;
#7759=CARTESIAN_POINT ( 'NONE',  ( -1.050138139902704104, -0.7221301030214424266, 0.000000000000000000 ) ) ;
#7762=DIRECTION ( 'NONE',  ( -0.2323175946639494671, 0.9726399823210830631, 0.000000000000000000 ) ) ;
#7768=CARTESIAN_POINT ( 'NONE',  ( 0.000000000000000000, 0.000000000000000000, 0.000000000000000000 ) ) ;
#7769=DIRECTION ( 'NONE',  ( -0.7879377495398138809, -0.6157549048526804736, 0.000000000000000000 ) ) ;
#7770=CARTESIAN_POINT ( 'NONE',  ( 1.240314151020239564, 1.658956310969643022, 0.2179999999999999993 ) ) ;
#7774=PLANE ( 'NONE',  #2652 ) ;
#7778=CARTESIAN_POINT ( 'NONE',  ( 1.349372409038269716, 1.744182786447574296, 0.1909097557292625813 ) ) ;
#7780=DIRECTION ( 'NONE',  ( 0.7879377495398137699, 0.6157549048526805846, 0.000000000000000000 ) ) ;
#7783=CARTESIAN_POINT ( 'NONE',  ( 1.363867297305675796, 1.069133023682674377, -0.1341576936804522446 ) ) ;
#7786=EDGE_CURVE ( 'NONE', #1048, #7184, #4766, .T. ) ;
#7788=CARTESIAN_POINT ( 'NONE',  ( 1.437142212823555587, 1.212327995211809117, 0.2500000000000000000 ) ) ;
#7791=ORIENTED_EDGE ( 'NONE', *, *, #4988, .F. ) ;
#7792=VECTOR ( 'NONE', #6662, 39.37007874015748143 ) ;
#7794=CARTESIAN_POINT ( 'NONE',  ( 1.493916101511090444, 1.213727529553185303, 0.2318685029578917700 ) ) ;
#7797=VERTEX_POINT ( 'NONE', #5872 ) ;
#7798=ORIENTED_EDGE ( 'NONE', *, *, #3925, .F. ) ;
#7799=CARTESIAN_POINT ( 'NONE',  ( -4.790174522854136363, -3.094341753229061798, 0.2179999999999999993 ) ) ;
#7800=DIRECTION ( 'NONE',  ( -0.4606913525677331367, -0.8875604078987031631, -0.000000000000000000 ) ) ;
#7803=CIRCLE ( 'NONE', #4278, 4.032000000000000917 ) ;
#7805=CIRCLE ( 'NONE', #6508, 0.4070000000000000839 ) ;
#7808=ORIENTED_EDGE ( 'NONE', *, *, #2587, .F. ) ;
#7816=EDGE_LOOP ( 'NONE', ( #4866, #5013, #4808, #4924 ) ) ;
#7818=CARTESIAN_POINT ( 'NONE',  ( 0.8135394388129588705, 1.284829519251779573, 0.03200000000000000067 ) ) ;
#7825=VERTEX_POINT ( 'NONE', #4367 ) ;
#7828=CARTESIAN_POINT ( 'NONE',  ( 1.457766515874196811, 1.224760407095971892, 0.2500000000000000000 ) ) ;
#7831=EDGE_CURVE ( 'NONE', #225, #3595, #485, .T. ) ;
#7832=ORIENTED_EDGE ( 'NONE', *, *, #6143, .T. ) ;
#7833=DIRECTION ( 'NONE',  ( -0.6157549048526729241, 0.7879377495398196540, 0.000000000000000000 ) ) ;
#7837=ADVANCED_FACE ( 'NONE', ( #2471 ), #1741, .F. ) ;
#7838=EDGE_CURVE ( 'NONE', #2698, #7979, #4549, .T. ) ;
#7845=CARTESIAN_POINT ( 'NONE',  ( -6.057578121783967262, -1.099253028489540318, -0.05999999999999999778 ) ) ;
#7847=CARTESIAN_POINT ( 'NONE',  ( -6.163625881728066247, -1.710116247721755522, 0.3125000000000000000 ) ) ;
#7849=DIRECTION ( 'NONE',  ( 0.6424495419751342640, 0.000000000000000000, 0.7663279885375060552 ) ) ;
#7851=DIRECTION ( 'NONE',  ( -0.000000000000000000, -0.000000000000000000, -1.000000000000000000 ) ) ;
#7854=ORIENTED_EDGE ( 'NONE', *, *, #5488, .F. ) ;
#7856=CARTESIAN_POINT ( 'NONE',  ( 1.142655413120957197, 0.6307864494084283180, 0.2179999999999999993 ) ) ;
#7857=CARTESIAN_POINT ( 'NONE',  ( 1.535624491898250898, 1.849481840152294998, -0.03984540547275473854 ) ) ;
#7860=CARTESIAN_POINT ( 'NONE',  ( 1.491488457038117721, 1.855243150880289349, -0.01042660034413028965 ) ) ;
#7861=PRODUCT_DEFINITION_SHAPE ( 'NONE', 'NONE',  #7594 ) ;
#7862=CARTESIAN_POINT ( 'NONE',  ( 1.498670457054695593, 1.228438162154884994, 0.2499999999999999722 ) ) ;
#7864=ORIENTED_EDGE ( 'NONE', *, *, #2587, .T. ) ;
#7865=CARTESIAN_POINT ( 'NONE',  ( 1.860542729474518930, 1.462361520562285744, -0.01844159883874913960 ) ) ;
#7866=CARTESIAN_POINT ( 'NONE',  ( 1.398758354407434235, 1.188821195468423131, 0.2500000000000000000 ) ) ;
#7875=EDGE_CURVE ( 'NONE', #6943, #518, #2435, .T. ) ;
#7876=LINE ( 'NONE', #2269, #3332 ) ;
#7887=ORIENTED_EDGE ( 'NONE', *, *, #2188, .T. ) ;
#7898=FACE_OUTER_BOUND ( 'NONE', #7552, .T. ) ;
#7900=VERTEX_POINT ( 'NONE', #6096 ) ;
#7905=CARTESIAN_POINT ( 'NONE',  ( 1.546772504294347428, 1.265727676674507585, 0.2500000000000104916 ) ) ;
#7906=VERTEX_POINT ( 'NONE', #1130 ) ;
#7914=ORIENTED_EDGE ( 'NONE', *, *, #5386, .T. ) ;
#7917=DIRECTION ( 'NONE',  ( 0.000000000000000000, 0.000000000000000000, 1.000000000000000000 ) ) ;
#7924=AXIS2_PLACEMENT_3D ( 'NONE', #4752, #6596, #5940 ) ;
#7927=CARTESIAN_POINT ( 'NONE',  ( 1.551450996633589874, 1.150725612071006987, 0.1733116977521490798 ) ) ;
#7929=DIRECTION ( 'NONE',  ( 0.7879377495398139919, 0.6157549048526803626, 0.000000000000000000 ) ) ;
#7937=LINE ( 'NONE', #1800, #6251 ) ;
#7948=CARTESIAN_POINT ( 'NONE',  ( -4.882388066182508091, 5.670153330992292240, 0.2500000000000000000 ) ) ;
#7955=PLANE ( 'NONE',  #4376 ) ;
#7956=CARTESIAN_POINT ( 'NONE',  ( 0.1028096983035128309, -0.4582465879184304258, 0.2187868247782020770 ) ) ;
#7959=ORIENTED_EDGE ( 'NONE', *, *, #1141, .F. ) ;
#7960=ORIENTED_EDGE ( 'NONE', *, *, #5837, .T. ) ;
#7963=CYLINDRICAL_SURFACE ( 'NONE', #2803, 0.3750000000000000555 ) ;
#7965=DIRECTION ( 'NONE',  ( 0.6157549048526801405, -0.7879377495398139919, 0.000000000000000000 ) ) ;
#7966=CARTESIAN_POINT ( 'NONE',  ( 1.535739741337429853, 1.855487842895053419, -3.030643867971292100E-16 ) ) ;
#7976=CARTESIAN_POINT ( 'NONE',  ( 1.302790242782180918, 1.667167568704493341, -0.1039999999999998703 ) ) ;
#7979=VERTEX_POINT ( 'NONE', #4942 ) ;
#7982=LINE ( 'NONE', #1721, #5322 ) ;
#7983=VERTEX_POINT ( 'NONE', #5015 ) ;
#7987=EDGE_LOOP ( 'NONE', ( #3025, #7306, #5320, #8060 ) ) ;
#8002=CARTESIAN_POINT ( 'NONE',  ( -4.790174522854136363, -3.094341753229061798, 0.000000000000000000 ) ) ;
#8005=CARTESIAN_POINT ( 'NONE',  ( 1.594422663808446217, 1.192243756349470551, 0.1923732503636950975 ) ) ;
#8011=CARTESIAN_POINT ( 'NONE',  ( 1.272999066882351205, 1.052213837524887508, -0.07009719302410664932 ) ) ;
#8013=AXIS2_PLACEMENT_3D ( 'NONE', #1337, #1260, #5737 ) ;
#8014=CARTESIAN_POINT ( 'NONE',  ( -6.110602001756019419, -1.404684638105634820, 0.2500000000000000000 ) ) ;
#8024=EDGE_CURVE ( 'NONE', #7415, #4011, #2373, .T. ) ;
#8025=AXIS2_PLACEMENT_3D ( 'NONE', #4417, #6912, #1247 ) ;
#8026=EDGE_CURVE ( 'NONE', #2111, #1048, #3945, .T. ) ;
#8028=ORIENTED_EDGE ( 'NONE', *, *, #823, .T. ) ;
#8029=DIRECTION ( 'NONE',  ( 1.000000000000000000, 0.000000000000000000, 0.000000000000000000 ) ) ;
#8034=CYLINDRICAL_SURFACE ( 'NONE', #2416, 0.03200000000000003536 ) ;
#8036=AXIS2_PLACEMENT_3D ( 'NONE', #5495, #3655, #529 ) ;
#8038=CARTESIAN_POINT ( 'NONE',  ( 0.2796912674003787513, -4.528516545235624413, 0.03199999999999999373 ) ) ;
#8040=CARTESIAN_POINT ( 'NONE',  ( 0.09071608944134439134, -0.4599287527268067777, 0.02334334155383705270 ) ) ;
#8043=FACE_OUTER_BOUND ( 'NONE', #4608, .T. ) ;
#8051=CIRCLE ( 'NONE', #4534, 3.939999999999463487 ) ;
#8053=EDGE_LOOP ( 'NONE', ( #5968, #5458, #1732, #2255 ) ) ;
#8054=CARTESIAN_POINT ( 'NONE',  ( 1.591124618940792157, 1.197007719324126640, 0.1929411818709917681 ) ) ;
#8058=LINE ( 'NONE', #6239, #1269 ) ;
#8060=ORIENTED_EDGE ( 'NONE', *, *, #872, .F. ) ;
#8063=AXIS2_PLACEMENT_3D ( 'NONE', #6136, #7917, #7443 ) ;
#8064=DIRECTION ( 'NONE',  ( 0.7879377495398141029, 0.6157549048526801405, 0.000000000000000000 ) ) ;
#8066=CARTESIAN_POINT ( 'NONE',  ( 1.723083782080649939, 1.395997476760423961, 0.1965221205739769994 ) ) ;
#8073=CARTESIAN_POINT ( 'NONE',  ( 1.571814533976804151, 1.273076930690908437, 0.2372021369714001904 ) ) ;
#8075=FACE_OUTER_BOUND ( 'NONE', #1952, .T. ) ;
#8078=DIRECTION ( 'NONE',  ( -0.000000000000000000, -0.000000000000000000, 1.000000000000000000 ) ) ;
#8085=CARTESIAN_POINT ( 'NONE',  ( 1.530682660343759327, 1.858020273156397284, -0.04707677864884684399 ) ) ;
#8088=CARTESIAN_POINT ( 'NONE',  ( 1.645823524873871069, 1.331476452140092581, 0.2367343346927103520 ) ) ;
#8122=COLOUR_RGB('Slate Gray', 0.72549020, 0.75294118, 0.79215686);
#8123=FILL_AREA_STYLE_COLOUR('',#8122);
#8124=FILL_AREA_STYLE('',(#8123));
#8125=SURFACE_STYLE_FILL_AREA(#8124);
#8126=SURFACE_SIDE_STYLE('',(#8125));
#8127=SURFACE_STYLE_USAGE(.BOTH.,#8126);
#8128=PRESENTATION_STYLE_ASSIGNMENT((#8127));
#8152=STYLED_ITEM('',(#8128),#3690);
#8153=MECHANICAL_DESIGN_GEOMETRIC_PRESENTATION_REPRESENTATION('',(#8152),#2249);
ENDSEC;
END-ISO-10303-21;
